ISO-10303-21;
HEADER;
FILE_DESCRIPTION (('STEP AP214'),
    '1' );
FILE_NAME ('6. Link.step',
    '2026-10-09T14:04:53',
    ( '' ),
    ( '' ),
    'SwSTEP 2.0',
    'SolidWorks 2021',
    '' );
FILE_SCHEMA (( 'AUTOMOTIVE_DESIGN' ));
ENDSEC;

DATA;
#39=ORIENTED_EDGE ( 'NONE', *, *, #35413, .T. ) ;
#91=CARTESIAN_POINT ( 'NONE',  ( 9.439578326262994423, 141.9252321839387037, 5.000000000000000000 ) ) ;
#131=EDGE_CURVE ( 'NONE', #70327, #36785, #1175, .T. ) ;
#134=SURFACE_SIDE_STYLE ('',( #74048 ) ) ;
#138=AXIS2_PLACEMENT_3D ( 'NONE', #88409, #103516, #29670 ) ;
#141=COLOUR_RGB ( '', 0.09019608, 0.27058824, 0.51372549) ;
#248=CARTESIAN_POINT ( 'NONE',  ( -5.901355035747913647, 4.636240438707916134, 5.000000000000000000 ) ) ;
#260=CARTESIAN_POINT ( 'NONE',  ( -6.617290780772931313, 5.039644235285652307, 4.935407925509285754 ) ) ;
#293=CARTESIAN_POINT ( 'NONE',  ( 3.021254343616667892, 47.67943487759343668, -5.000000000000000000 ) ) ;
#379=MECHANICAL_DESIGN_GEOMETRIC_PRESENTATION_REPRESENTATION('',(#26349),#84892);
#521=FILL_AREA_STYLE ('',( #34037 ) ) ;
#614=ORIENTED_EDGE ( 'NONE', *, *, #97880, .F. ) ;
#727=CIRCLE ( 'NONE', #54110, 10.00000000000000000 ) ;
#788=CARTESIAN_POINT ( 'NONE',  ( -8.628857352971980532, 6.504966632935141213, 3.765103137054122584 ) ) ;
#790=STYLED_ITEM ( 'NONE', ( #43828 ), #87638 ) ;
#854=ORIENTED_EDGE ( 'NONE', *, *, #81130, .F. ) ;
#1175=B_SPLINE_CURVE_WITH_KNOTS ( 'NONE', 3,
 ( #75129, #68117, #101015, #76730, #90813, #1225, #34192, #2843, #27169, #60060, #16928, #8814, #49805, #82711, #26123, #66528, #58979, #45979, #3391, #101554, #102616, #77813, #61653, #29819, #3924, #103151, #93993, #54035, #27710, #95589, #44929, #94543, #54567, #61105, #62697, #20153, #13049, #37389, #12521, #53533, #86979, #21205, #11458, #85925 ),
 .UNSPECIFIED., .F., .F.,
 ( 4, 2, 2, 2, 2, 2, 2, 2, 2, 2, 2, 2, 2, 2, 2, 2, 2, 2, 2, 2, 2, 4 ),
 ( 0.000000000000000000, 0.0005557066357529374858, 0.001111413271505874972, 0.002222826543011752545, 0.003334239814517629685, 0.004445653086023509427, 0.006668479629035269779, 0.008891306172047029263, 0.01333695925807055517, 0.01778261234409407934, 0.02667391851614113810, 0.03556522468818819338, 0.05334783703228231089, 0.07113044937637644227, 0.08891306172047055978, 0.1066956740645646912, 0.1155869802366117499, 0.1244782864086588087, 0.1333695925807058813, 0.1378152456667294246, 0.1400380722097411823, 0.1422608987527529401 ),
 .UNSPECIFIED. ) ;
#1195=( NAMED_UNIT ( * ) PLANE_ANGLE_UNIT ( ) SI_UNIT ( $, .RADIAN. ) );
#1196=CARTESIAN_POINT ( 'NONE',  ( -10.03463480799100438, 7.450536368003699117, 0.000000000000000000 ) ) ;
#1225=CARTESIAN_POINT ( 'NONE',  ( -5.249407336941563251, 5.831820959896639067, -5.000000000000000000 ) ) ;
#1254=VERTEX_POINT ( 'NONE', #49424 ) ;
#1352=VERTEX_POINT ( 'NONE', #11622 ) ;
#1375=CARTESIAN_POINT ( 'NONE',  ( 4.258999010316228073, 11.59408722316739038, -5.000000000000002665 ) ) ;
#1444=DIRECTION ( 'NONE',  ( -0.000000000000000000, -1.000000000000000000, -0.000000000000000000 ) ) ;
#1462=CARTESIAN_POINT ( 'NONE',  ( -3.067650313623253577, 44.37499570395408455, 5.000000000000000000 ) ) ;
#1467=DIRECTION ( 'NONE',  ( 0.000000000000000000, 0.000000000000000000, 1.000000000000000000 ) ) ;
#1625=CARTESIAN_POINT ( 'NONE',  ( 6.231493956936416723, 147.8264543773111654, -5.000000000000000000 ) ) ;
#1627=DIRECTION ( 'NONE',  ( 1.000000000000000000, 0.000000000000000000, 0.000000000000000000 ) ) ;
#1692=CARTESIAN_POINT ( 'NONE',  ( 14.54015256618498775, 9.738273119607207207, 0.000000000000000000 ) ) ;
#1746=CARTESIAN_POINT ( 'NONE',  ( -9.999806008763298948, 7.500277120283445953, -4.999999999999999112 ) ) ;
#1760=FACE_OUTER_BOUND ( 'NONE', #32612, .T. ) ;
#1829=ORIENTED_EDGE ( 'NONE', *, *, #76927, .F. ) ;
#1914=CARTESIAN_POINT ( 'NONE',  ( 4.678819457397416670, 143.9212778189090614, -5.000000000000000000 ) ) ;
#1918=CARTESIAN_POINT ( 'NONE',  ( 3.443309072005564797, 27.85918987796394575, -5.000000000000000000 ) ) ;
#1922=AXIS2_PLACEMENT_3D ( 'NONE', #72176, #95393, #5838 ) ;
#1954=UNCERTAINTY_MEASURE_WITH_UNIT (LENGTH_MEASURE( 1.000000000000000082E-05 ), #85242, 'distance_accuracy_value', 'NONE');
#1999=CARTESIAN_POINT ( 'NONE',  ( -3.572097512798535046, 127.8538299566993004, 5.000000000000000888 ) ) ;
#2022=LINE ( 'NONE', #59222, #39129 ) ;
#2100=CARTESIAN_POINT ( 'NONE',  ( 8.830661707197901222, 133.7962572603164801, 8.673617379768678370E-16 ) ) ;
#2101=ORIENTED_EDGE ( 'NONE', *, *, #75261, .T. ) ;
#2246=CARTESIAN_POINT ( 'NONE',  ( 0.000000000000000000, 0.000000000000000000, -5.000000000000000000 ) ) ;
#2257=( GEOMETRIC_REPRESENTATION_CONTEXT ( 3 ) GLOBAL_UNCERTAINTY_ASSIGNED_CONTEXT ( ( #66150 ) ) GLOBAL_UNIT_ASSIGNED_CONTEXT ( ( #55188, #55705, #106391 ) ) REPRESENTATION_CONTEXT ( 'NONE', 'WORKASPACE' ) );
#2274=CARTESIAN_POINT ( 'NONE',  ( -6.072471596195612165, 4.391857883210726676, -5.000000000000000000 ) ) ;
#2290=DIRECTION ( 'NONE',  ( -1.000000000000000000, 0.000000000000000000, 0.000000000000000000 ) ) ;
#2341=STYLED_ITEM ( 'NONE', ( #80001 ), #51084 ) ;
#2407=CARTESIAN_POINT ( 'NONE',  ( 12.50000000000000000, 1.530808498934191521E-15, 0.000000000000000000 ) ) ;
#2539=CARTESIAN_POINT ( 'NONE',  ( -3.242641670810647803, 35.58872425396818073, 5.000000000000000000 ) ) ;
#2611=DIRECTION ( 'NONE',  ( -1.000000000000000000, 0.000000000000000000, 0.000000000000000000 ) ) ;
#2639=CARTESIAN_POINT ( 'NONE',  ( 8.361479372587984571, 121.1764542251201249, 0.000000000000000000 ) ) ;
#2698=EDGE_CURVE ( 'NONE', #37342, #96258, #37652, .T. ) ;
#2710=EDGE_CURVE ( 'NONE', #12734, #106589, #8348, .T. ) ;
#2785=UNCERTAINTY_MEASURE_WITH_UNIT (LENGTH_MEASURE( 1.000000000000000082E-05 ), #98574, 'distance_accuracy_value', 'NONE');
#2791=DIRECTION ( 'NONE',  ( -1.000000000000000000, 0.000000000000000000, 0.000000000000000000 ) ) ;
#2799=AXIS2_PLACEMENT_3D ( 'NONE', #15203, #105805, #48091 ) ;
#2816=SURFACE_STYLE_FILL_AREA ( #76705 ) ;
#2817=( NAMED_UNIT ( * ) PLANE_ANGLE_UNIT ( ) SI_UNIT ( $, .RADIAN. ) );
#2843=CARTESIAN_POINT ( 'NONE',  ( -4.921285567847696107, 6.866253350555239443, -5.000000000000000000 ) ) ;
#2982=DIRECTION ( 'NONE',  ( 0.000000000000000000, 0.000000000000000000, -1.000000000000000000 ) ) ;
#3040=ORIENTED_EDGE ( 'NONE', *, *, #91556, .T. ) ;
#3079=CARTESIAN_POINT ( 'NONE',  ( -8.813577900734397730, 133.4610148809356929, 4.999999999999998224 ) ) ;
#3186=CARTESIAN_POINT ( 'NONE',  ( 7.869427812662803667, 64.69537499113458523, -2.456618345357718155E-12 ) ) ;
#3197=DIRECTION ( 'NONE',  ( 1.000000000000000000, 0.000000000000000000, 0.000000000000000000 ) ) ;
#3219=( GEOMETRIC_REPRESENTATION_CONTEXT ( 3 ) GLOBAL_UNCERTAINTY_ASSIGNED_CONTEXT ( ( #23648 ) ) GLOBAL_UNIT_ASSIGNED_CONTEXT ( ( #10926, #85379, #51401 ) ) REPRESENTATION_CONTEXT ( 'NONE', 'WORKASPACE' ) );
#3260=VERTEX_POINT ( 'NONE', #46300 ) ;
#3292=CARTESIAN_POINT ( 'NONE',  ( -8.182558299557642911, 38.50572386936678271, -0.000000000000000000 ) ) ;
#3366=CARTESIAN_POINT ( 'NONE',  ( -8.473474469297077150, 27.00279687855394428, 0.000000000000000000 ) ) ;
#3391=CARTESIAN_POINT ( 'NONE',  ( -3.727646769453142106, 20.26854631371922366, -5.000000000000000000 ) ) ;
#3392=CARTESIAN_POINT ( 'NONE',  ( 7.849086896546205061, 81.65194826718307297, -4.999999999990173194 ) ) ;
#3397=PRESENTATION_STYLE_ASSIGNMENT (( #8289 ) ) ;
#3622=CARTESIAN_POINT ( 'NONE',  ( -2.856172004554211608, 67.80853407705139091, 5.000000000000000000 ) ) ;
#3728=CARTESIAN_POINT ( 'NONE',  ( 9.240146679350036862, 139.9709698506905795, 5.000000000000307310 ) ) ;
#3758=( GEOMETRIC_REPRESENTATION_CONTEXT ( 3 ) GLOBAL_UNCERTAINTY_ASSIGNED_CONTEXT ( ( #57126 ) ) GLOBAL_UNIT_ASSIGNED_CONTEXT ( ( #84072, #9103, #100777 ) ) REPRESENTATION_CONTEXT ( 'NONE', 'WORKASPACE' ) );
#3773=( NAMED_UNIT ( * ) SI_UNIT ( $, .STERADIAN. ) SOLID_ANGLE_UNIT ( ) );
#3791=EDGE_LOOP ( 'NONE', ( #104575, #33041, #72543, #65147 ) ) ;
#3828=CARTESIAN_POINT ( 'NONE',  ( -9.755167981113400444, 8.162422641044738469, 0.000000000000000000 ) ) ;
#3842=ORIENTED_EDGE ( 'NONE', *, *, #34582, .T. ) ;
#3881=EDGE_CURVE ( 'NONE', #55300, #30328, #51787, .T. ) ;
#3896=CARTESIAN_POINT ( 'NONE',  ( -7.989277284034971949, 50.32447066040694494, -4.999999999999999112 ) ) ;
#3924=CARTESIAN_POINT ( 'NONE',  ( -2.983112692022612311, 50.82233998752811743, -5.000000000000000888 ) ) ;
#4093=UNCERTAINTY_MEASURE_WITH_UNIT (LENGTH_MEASURE( 1.000000000000000082E-05 ), #55373, 'distance_accuracy_value', 'NONE');
#4106=STYLED_ITEM ( 'NONE', ( #89358 ), #85004 ) ;
#4152=CARTESIAN_POINT ( 'NONE',  ( -9.252395038628018042, 11.88928468659940307, 0.000000000000000000 ) ) ;
#4257=CARTESIAN_POINT ( 'NONE',  ( 7.500000000000006217, 152.0000000000000000, 0.000000000000000000 ) ) ;
#4261=DIRECTION ( 'NONE',  ( 0.000000000000000000, 0.000000000000000000, 1.000000000000000000 ) ) ;
#4322=PRESENTATION_STYLE_ASSIGNMENT (( #37790 ) ) ;
#4393=CARTESIAN_POINT ( 'NONE',  ( 7.849088119671323582, 81.59499423012449881, 1.301042606982605321E-15 ) ) ;
#4421=CARTESIAN_POINT ( 'NONE',  ( -9.832775749609577787, 7.875845744895693556, 0.000000000000000000 ) ) ;
#4446=CARTESIAN_POINT ( 'NONE',  ( 9.609486011791064541, 143.0915023496501419, -5.000000000000000888 ) ) ;
#4568=PRODUCT_DEFINITION_SHAPE ( 'NONE', 'NONE',  #12664 ) ;
#4648=DIRECTION ( 'NONE',  ( 0.000000000000000000, 0.000000000000000000, -1.000000000000000000 ) ) ;
#4685=CARTESIAN_POINT ( 'NONE',  ( -9.692620405620905544, 8.443756516928340616, 4.999999999999841904 ) ) ;
#4764=( GEOMETRIC_REPRESENTATION_CONTEXT ( 3 ) GLOBAL_UNCERTAINTY_ASSIGNED_CONTEXT ( ( #69890 ) ) GLOBAL_UNIT_ASSIGNED_CONTEXT ( ( #75813, #10013, #42377 ) ) REPRESENTATION_CONTEXT ( 'NONE', 'WORKASPACE' ) );
#4827=DIRECTION ( 'NONE',  ( -1.000000000000000000, 0.000000000000000000, 0.000000000000000000 ) ) ;
#4848=B_SPLINE_CURVE_WITH_KNOTS ( 'NONE', 3,
 ( #38338, #20603, #37822, #86362, #77182, #103574, #103056, #94445, #52906, #87409, #28136, #71199, #63122, #53945, #86880, #20054, #46408, #62598, #85826, #104094, #21627, #3292, #12426, #77717, #61014, #30234, #11903, #36233, #54457, #69105, #70153, #69629, #101975, #44830, #3828, #102522, #88984, #6986, #63664, #66705 ),
 .UNSPECIFIED., .F., .F.,
 ( 4, 2, 2, 2, 2, 2, 2, 2, 2, 2, 2, 2, 2, 2, 2, 2, 2, 2, 2, 4 ),
 ( 2.797157557069881010E-17, 0.002121099353757972556, 0.004242198707515917357, 0.008484397415031806958, 0.01696879483006366943, 0.02545319224509545036, 0.03393758966012722783, 0.05090638449019078277, 0.06787517932025434464, 0.08484397415031789957, 0.1018127689803814268, 0.1102971663954131903, 0.1187815638104449539, 0.1272659612254767036, 0.1315081599329925577, 0.1336292592867505125, 0.1346898089636294760, 0.1352200838020689577, 0.1354852212212886986, 0.1357503586405084395 ),
 .UNSPECIFIED. ) ;
#4884=CARTESIAN_POINT ( 'NONE',  ( -14.54015256618497176, 142.2617268803927573, 0.000000000000000000 ) ) ;
#4927=CIRCLE ( 'NONE', #65188, 5.000000000000000000 ) ;
#4933=CARTESIAN_POINT ( 'NONE',  ( 9.493007256569747199, 142.3993658332746577, -0.000000000000000000 ) ) ;
#4944=CIRCLE ( 'NONE', #44611, 10.00000000000000000 ) ;
#4959=CARTESIAN_POINT ( 'NONE',  ( -4.455300429064767975, 9.670763880908177512, -5.000000000000000888 ) ) ;
#4973=CYLINDRICAL_SURFACE ( 'NONE', #84155, 5.000000000000002665 ) ;
#4988=CARTESIAN_POINT ( 'NONE',  ( 3.646183794689596969, 129.8030994959483735, -4.999999999999999112 ) ) ;
#5161=DIRECTION ( 'NONE',  ( -1.000000000000000000, 0.000000000000000000, 0.000000000000000000 ) ) ;
#5177=DIRECTION ( 'NONE',  ( -1.000000000000000000, 0.000000000000000000, 0.000000000000000000 ) ) ;
#5213=CARTESIAN_POINT ( 'NONE',  ( -9.743481593188134227, 8.211523606429958377, 5.000000000000000888 ) ) ;
#5217=DIRECTION ( 'NONE',  ( 1.000000000000000000, 0.000000000000000000, 0.000000000000000000 ) ) ;
#5458=CARTESIAN_POINT ( 'NONE',  ( 9.269852382678077873, 11.68551705847642275, -0.000000000000000000 ) ) ;
#5484=CARTESIAN_POINT ( 'NONE',  ( -8.308397487264409520, 32.82220968432262964, 0.000000000000000000 ) ) ;
#5511=CARTESIAN_POINT ( 'NONE',  ( 2.955796066023817836, 98.65787461558377913, -5.000000000000000888 ) ) ;
#5566=CARTESIAN_POINT ( 'NONE',  ( 3.591870599023073485, 23.61213490889384659, 5.000000000000000000 ) ) ;
#5692=ORIENTED_EDGE ( 'NONE', *, *, #37906, .F. ) ;
#5727=CARTESIAN_POINT ( 'NONE',  ( -9.880470762086103420, 7.740809968950301823, 5.000000000000000888 ) ) ;
#5767=( LENGTH_UNIT ( ) NAMED_UNIT ( * ) SI_UNIT ( .MILLI., .METRE. ) );
#5792=EDGE_CURVE ( 'NONE', #52915, #44815, #4944, .T. ) ;
#5830=CARTESIAN_POINT ( 'NONE',  ( 9.609486011791425142, 143.0915023496523020, 5.000000000000000888 ) ) ;
#5838=DIRECTION ( 'NONE',  ( 1.000000000000000000, 0.000000000000000000, 0.000000000000000000 ) ) ;
#5848=ORIENTED_EDGE ( 'NONE', *, *, #40738, .T. ) ;
#5849=TOROIDAL_SURFACE ( 'NONE', #36931, 10.00000000000000000, 5.000000000000000000 ) ;
#5919=DIRECTION ( 'NONE',  ( 0.000000000000000000, 0.000000000000000000, -1.000000000000000000 ) ) ;
#5999=CARTESIAN_POINT ( 'NONE',  ( -7.856068184142580790, 67.85260481710604097, -5.000000000005080381 ) ) ;
#6019=ORIENTED_EDGE ( 'NONE', *, *, #95117, .T. ) ;
#6026=CARTESIAN_POINT ( 'NONE',  ( 8.167412539197350441, 39.27912669871957263, 1.228248305376115968E-12 ) ) ;
#6042=EDGE_LOOP ( 'NONE', ( #12347, #26136, #28707, #104471 ) ) ;
#6093=DIRECTION ( 'NONE',  ( 0.000000000000000000, 0.000000000000000000, -1.000000000000000000 ) ) ;
#6110=( NAMED_UNIT ( * ) PLANE_ANGLE_UNIT ( ) SI_UNIT ( $, .RADIAN. ) );
#6157=SURFACE_SIDE_STYLE ('',( #62308 ) ) ;
#6242=CARTESIAN_POINT ( 'NONE',  ( -5.171846360987437663, 6.036654300442626742, 5.000000000000000000 ) ) ;
#6351=CARTESIAN_POINT ( 'NONE',  ( -3.727843730184232207, 20.26410795673177745, 4.999999999999997335 ) ) ;
#6363=AXIS2_PLACEMENT_3D ( 'NONE', #65929, #100948, #83693 ) ;
#6497=CARTESIAN_POINT ( 'NONE',  ( 7.869023716279121672, 87.19016966530782042, -2.311115933264685126E-30 ) ) ;
#6523=CARTESIAN_POINT ( 'NONE',  ( -8.420691126292242146, 123.3228360287979797, -5.000000000001269207 ) ) ;
#6526=EDGE_CURVE ( 'NONE', #24323, #37342, #49888, .T. ) ;
#6547=DIRECTION ( 'NONE',  ( -1.000000000000000000, 0.000000000000000000, 0.000000000000000000 ) ) ;
#6553=CARTESIAN_POINT ( 'NONE',  ( 4.086538315195368476, 13.70928807340287747, -5.000000000000000000 ) ) ;
#6594=ORIENTED_EDGE ( 'NONE', *, *, #59211, .T. ) ;
#6622=CARTESIAN_POINT ( 'NONE',  ( 4.322723262675009614, 10.88947096379691715, 5.000000000000002665 ) ) ;
#6768=MECHANICAL_DESIGN_GEOMETRIC_PRESENTATION_REPRESENTATION('',(#72207),#39719);
#6787=CARTESIAN_POINT ( 'NONE',  ( -10.04820350651657357, 7.431158258250301074, 4.999999999999990230 ) ) ;
#6824=( NAMED_UNIT ( * ) PLANE_ANGLE_UNIT ( ) SI_UNIT ( $, .RADIAN. ) );
#6828=CARTESIAN_POINT ( 'NONE',  ( 4.322615621094081817, 141.1094294873553849, -4.999999999999998224 ) ) ;
#6936=SURFACE_SIDE_STYLE ('',( #70626 ) ) ;
#6986=CARTESIAN_POINT ( 'NONE',  ( -9.914196165181285991, 7.656226977557262892, -0.000000000000000000 ) ) ;
#6997=CARTESIAN_POINT ( 'NONE',  ( -4.678819457397405124, 143.9212778189090045, 0.000000000000000000 ) ) ;
#7057=CARTESIAN_POINT ( 'NONE',  ( -7.939742226420592353, 97.07168777242631563, -5.080791182465135870E-12 ) ) ;
#7123=MECHANICAL_DESIGN_GEOMETRIC_PRESENTATION_REPRESENTATION('',(#72574),#65725);
#7149=CARTESIAN_POINT ( 'NONE',  ( 3.768804542112334399, 19.36671096900046152, 5.000000000000000000 ) ) ;
#7173=CARTESIAN_POINT ( 'NONE',  ( 3.363233428609793130, 121.3096164343346999, 4.999999999999998224 ) ) ;
#7186=ORIENTED_EDGE ( 'NONE', *, *, #46079, .F. ) ;
#7303=CARTESIAN_POINT ( 'NONE',  ( 0.000000000000000000, 0.000000000000000000, 5.000000000000000000 ) ) ;
#7308=CARTESIAN_POINT ( 'NONE',  ( -14.54015256618497176, 142.2617268803927573, 0.000000000000000000 ) ) ;
#7334=COLOUR_RGB ( '', 0.08235294, 0.09019608, 0.10196078) ;
#7429=( NAMED_UNIT ( * ) PLANE_ANGLE_UNIT ( ) SI_UNIT ( $, .RADIAN. ) );
#7468=CARTESIAN_POINT ( 'NONE',  ( 7.500000000000007105, 152.0000000000000000, 5.000000000000000000 ) ) ;
#7565=AXIS2_PLACEMENT_3D ( 'NONE', #65932, #23374, #33062 ) ;
#7577=CARTESIAN_POINT ( 'NONE',  ( -9.434261306447488948, 141.8831429914396836, 0.000000000000000000 ) ) ;
#7609=CARTESIAN_POINT ( 'NONE',  ( 8.588478090878989946, 23.79665183991722799, -4.999999999999385381 ) ) ;
#7669=CARTESIAN_POINT ( 'NONE',  ( 4.258978623649388950, 11.59436199737384676, 5.000000000000000000 ) ) ;
#7699=( LENGTH_UNIT ( ) NAMED_UNIT ( * ) SI_UNIT ( .MILLI., .METRE. ) );
#7700=CARTESIAN_POINT ( 'NONE',  ( 4.678819457397886517, 143.9212778189118467, 5.000000000000000000 ) ) ;
#7739=DIRECTION ( 'NONE',  ( 0.5564727496918392413, -0.8308658609248571469, 0.000000000000000000 ) ) ;
#7835=CARTESIAN_POINT ( 'NONE',  ( 0.000000000000000000, 0.000000000000000000, 5.000000000000000000 ) ) ;
#7836=CARTESIAN_POINT ( 'NONE',  ( -10.16315516181093237, 7.266990280869978669, 0.000000000000000000 ) ) ;
#7851=CARTESIAN_POINT ( 'NONE',  ( -9.001830022268279663, 6.775897538200406522, 3.303914975154940148 ) ) ;
#7897=CARTESIAN_POINT ( 'NONE',  ( -9.864719719466185310, 7.401937201847157866, -1.292133144274320911 ) ) ;
#7912=VECTOR ( 'NONE', #91247, 1000.000000000000000 ) ;
#7952=CARTESIAN_POINT ( 'NONE',  ( 0.000000000000000000, 152.0000000000000000, 0.000000000000000000 ) ) ;
#7966=CARTESIAN_POINT ( 'NONE',  ( -4.468441761983152460, 142.4699803267851621, 5.000000000000002665 ) ) ;
#8158=CARTESIAN_POINT ( 'NONE',  ( 8.361479372589355918, 30.82354577482341895, -1.227442566772675775E-12 ) ) ;
#8216=CARTESIAN_POINT ( 'NONE',  ( 9.300689189976646176, 140.6377497889584447, 5.000000000000000000 ) ) ;
#8240=CARTESIAN_POINT ( 'NONE',  ( 3.641358249959614657, 129.8026804635382234, 5.000000000000000888 ) ) ;
#8289=SURFACE_STYLE_USAGE ( .BOTH. , #82173 ) ;
#8348=CIRCLE ( 'NONE', #41067, 7.500000000000000888 ) ;
#8375=CARTESIAN_POINT ( 'NONE',  ( -10.03543110037283093, 7.449399144625812319, 0.000000000000000000 ) ) ;
#8503=CARTESIAN_POINT ( 'NONE',  ( -9.229740628749548037, 139.8534222827520068, -1.734723476015833818E-15 ) ) ;
#8557=DIRECTION ( 'NONE',  ( 0.000000000000000000, 0.000000000000000000, -1.000000000000000000 ) ) ;
#8746=CARTESIAN_POINT ( 'NONE',  ( 8.167412539197048460, 112.7208733012629125, 0.000000000000000000 ) ) ;
#8814=CARTESIAN_POINT ( 'NONE',  ( -4.483615626739970494, 9.381785226897060070, -5.000000000000000000 ) ) ;
#8888=ORIENTED_EDGE ( 'NONE', *, *, #87726, .F. ) ;
#8994=ORIENTED_EDGE ( 'NONE', *, *, #79912, .T. ) ;
#9103=( NAMED_UNIT ( * ) PLANE_ANGLE_UNIT ( ) SI_UNIT ( $, .RADIAN. ) );
#9229=COLOUR_RGB ( '', 0.08235294, 0.09019608, 0.10196078) ;
#9251=PRESENTATION_STYLE_ASSIGNMENT (( #26040 ) ) ;
#9306=CARTESIAN_POINT ( 'NONE',  ( -9.993183759207806105, 7.509940706527443943, 0.000000000000000000 ) ) ;
#9393=( BOUNDED_SURFACE ( )  B_SPLINE_SURFACE ( 3, 2, ( 
 ( #56755, #63822, #23372 ),
 ( #72425, #80501, #79455 ),
 ( #39012, #64355, #104795 ),
 ( #97223, #22319, #6622 ),
 ( #39549, #105329, #7669 ),
 ( #14705, #31472, #72938 ),
 ( #89682, #22848, #15249 ),
 ( #15780, #48136, #40588 ),
 ( #81033, #48662, #7149 ),
 ( #79976, #71356, #106365 ),
 ( #40061, #81547, #5566 ),
 ( #104256, #32530, #30402 ),
 ( #57283, #63289, #96189 ),
 ( #96712, #55164, #30945 ),
 ( #88093, #47077, #55682 ),
 ( #93795, #52254, #28557 ),
 ( #26964, #77610, #84639 ),
 ( #3186, #68999, #92718 ),
 ( #85167, #59849, #44182 ),
 ( #76002, #90741, #18879 ),
 ( #16857, #49737, #19421 ),
 ( #43640, #98809, #11253 ),
 ( #76529, #61441, #94333 ),
 ( #8746, #101875, #35052 ),
 ( #51722, #28034, #10724 ),
 ( #2639, #93259, #82646 ),
 ( #77071, #57818, #35585 ),
 ( #102414, #68461, #36132 ),
 ( #27507, #24963, #43114 ),
 ( #49197, #101353, #60383 ),
 ( #2100, #60906, #67918 ),
 ( #19952, #52793, #85717 ),
 ( #100805, #41125, #11791 ),
 ( #44722, #3728, #82097 ),
 ( #36658, #8216, #69522 ),
 ( #74009, #91, #33060 ),
 ( #65930, #37722, #14438 ),
 ( #30140, #5830, #95921 ) ),
 .UNSPECIFIED., .F., .F., .F. ) 
 B_SPLINE_SURFACE_WITH_KNOTS ( ( 4, 2, 2, 2, 2, 2, 2, 2, 2, 2, 2, 2, 2, 2, 2, 2, 2, 2, 4 ),
 ( 3, 3 ),
 ( 0.06375477930561529449, 0.06591736287010073470, 0.06807994643458617490, 0.07240511356355705530, 0.07673028069252793570, 0.08105544782149880223, 0.08970578207944054916, 0.09835611633738230997, 0.1156567848532658177, 0.1329574533691493254, 0.1502581218850328193, 0.1675587904009163132, 0.1762091246588580740, 0.1848594589167998348, 0.1891846260457707152, 0.1935097931747415956, 0.1978349603037124482, 0.1999975438681979023, 0.2021601274326833286 ),
 ( 0.000000000000000000, 1.000000000000000000 ),
 .UNSPECIFIED. ) 
 GEOMETRIC_REPRESENTATION_ITEM ( )  RATIONAL_B_SPLINE_SURFACE ( (
 ( 1.000000000000000000, 0.7071067811865475727, 1.000000000000000000),
 ( 1.000000000000000000, 0.7071067811865475727, 1.000000000000000000),
 ( 1.000000000000000000, 0.7071067811865474617, 1.000000000000000000),
 ( 1.000000000000000000, 0.7071067811865474617, 1.000000000000000000),
 ( 1.000000000000000000, 0.7071067811865475727, 1.000000000000000000),
 ( 1.000000000000000000, 0.7071067811865475727, 1.000000000000000000),
 ( 1.000000000000000000, 0.7071067811865475727, 1.000000000000000000),
 ( 1.000000000000000000, 0.7071067811865475727, 1.000000000000000000),
 ( 1.000000000000000000, 0.7071067811865475727, 1.000000000000000000),
 ( 1.000000000000000000, 0.7071067811865475727, 1.000000000000000000),
 ( 1.000000000000000000, 0.7071067811865474617, 1.000000000000000000),
 ( 1.000000000000000000, 0.7071067811865474617, 1.000000000000000000),
 ( 1.000000000000000000, 0.7071067811865475727, 1.000000000000000000),
 ( 1.000000000000000000, 0.7071067811865475727, 1.000000000000000000),
 ( 1.000000000000000000, 0.7071067811865475727, 1.000000000000000000),
 ( 1.000000000000000000, 0.7071067811865475727, 1.000000000000000000),
 ( 1.000000000000000000, 0.7071067811865475727, 1.000000000000000000),
 ( 1.000000000000000000, 0.7071067811865475727, 1.000000000000000000),
 ( 1.000000000000000000, 0.7071067811865475727, 1.000000000000000000),
 ( 1.000000000000000000, 0.7071067811865475727, 1.000000000000000000),
 ( 1.000000000000000000, 0.7071067811865475727, 1.000000000000000000),
 ( 1.000000000000000000, 0.7071067811865475727, 1.000000000000000000),
 ( 1.000000000000000000, 0.7071067811865475727, 1.000000000000000000),
 ( 1.000000000000000000, 0.7071067811865475727, 1.000000000000000000),
 ( 1.000000000000000000, 0.7071067811865475727, 1.000000000000000000),
 ( 1.000000000000000000, 0.7071067811865475727, 1.000000000000000000),
 ( 1.000000000000000000, 0.7071067811865475727, 1.000000000000000000),
 ( 1.000000000000000000, 0.7071067811865475727, 1.000000000000000000),
 ( 1.000000000000000000, 0.7071067811865474617, 1.000000000000000000),
 ( 1.000000000000000000, 0.7071067811865474617, 1.000000000000000000),
 ( 1.000000000000000000, 0.7071067811865474617, 1.000000000000000000),
 ( 1.000000000000000000, 0.7071067811865474617, 1.000000000000000000),
 ( 1.000000000000000000, 0.7071067811865475727, 1.000000000000000000),
 ( 1.000000000000000000, 0.7071067811865475727, 1.000000000000000000),
 ( 1.000000000000000000, 0.7071067811865474617, 1.000000000000000000),
 ( 1.000000000000000000, 0.7071067811865474617, 1.000000000000000000),
 ( 1.000000000000000000, 0.7071067811865475727, 1.000000000000000000),
 ( 1.000000000000000000, 0.7071067811865475727, 1.000000000000000000) ) ) 
 REPRESENTATION_ITEM ( '' )  SURFACE ( )  );
#9466=FILL_AREA_STYLE_COLOUR ( '', #49553 ) ;
#9496=ADVANCED_FACE ( 'NONE', ( #58349 ), #90460, .T. ) ;
#9781=DIRECTION ( 'NONE',  ( -1.000000000000000000, 0.000000000000000000, 0.000000000000000000 ) ) ;
#9786=CARTESIAN_POINT ( 'NONE',  ( -12.50000000000000000, 0.000000000000000000, 0.000000000000000000 ) ) ;
#9839=( NAMED_UNIT ( * ) SI_UNIT ( $, .STERADIAN. ) SOLID_ANGLE_UNIT ( ) );
#9840=CARTESIAN_POINT ( 'NONE',  ( -9.999342726568489326, 7.500940813882568392, -5.000000000000000888 ) ) ;
#9891=EDGE_CURVE ( 'NONE', #91113, #3260, #69829, .T. ) ;
#10013=( NAMED_UNIT ( * ) PLANE_ANGLE_UNIT ( ) SI_UNIT ( $, .RADIAN. ) );
#10018=ORIENTED_EDGE ( 'NONE', *, *, #10109, .T. ) ;
#10047=UNCERTAINTY_MEASURE_WITH_UNIT (LENGTH_MEASURE( 1.000000000000000082E-05 ), #87876, 'distance_accuracy_value', 'NONE');
#10093=CARTESIAN_POINT ( 'NONE',  ( 4.678819457397413117, 143.9212778189090898, 0.000000000000000000 ) ) ;
#10103=CARTESIAN_POINT ( 'NONE',  ( -8.745545711797721111, 132.0170111787107317, 5.000000000000635936 ) ) ;
#10109=EDGE_CURVE ( 'NONE', #65330, #31480, #17632, .T. ) ;
#10145=VERTEX_POINT ( 'NONE', #13243 ) ;
#10190=EDGE_CURVE ( 'NONE', #74794, #83609, #26288, .T. ) ;
#10350=DIRECTION ( 'NONE',  ( -0.000000000000000000, -0.000000000000000000, 1.000000000000000000 ) ) ;
#10373=CARTESIAN_POINT ( 'NONE',  ( -10.43542583693973036, 6.878147458890449428, 0.000000000000000000 ) ) ;
#10625=CARTESIAN_POINT ( 'NONE',  ( -8.813577900860385839, 133.4610148809287864, -1.734723475955139846E-15 ) ) ;
#10714=DIRECTION ( 'NONE',  ( -1.000000000000000000, 0.000000000000000000, 0.000000000000000000 ) ) ;
#10724=CARTESIAN_POINT ( 'NONE',  ( 3.225607053687307602, 115.6489559503065152, 5.000000000000000000 ) ) ;
#10728=AXIS2_PLACEMENT_3D ( 'NONE', #14983, #57033, #47878 ) ;
#10865=ORIENTED_EDGE ( 'NONE', *, *, #16070, .F. ) ;
#10894=CARTESIAN_POINT ( 'NONE',  ( -9.999806008771985333, 7.500277120289516652, 0.000000000000000000 ) ) ;
#10915=VERTEX_POINT ( 'NONE', #54495 ) ;
#10926=( LENGTH_UNIT ( ) NAMED_UNIT ( * ) SI_UNIT ( .MILLI., .METRE. ) );
#11149=CARTESIAN_POINT ( 'NONE',  ( -8.147102310899050792, 111.6559345260857441, -1.270355265678086219E-12 ) ) ;
#11253=CARTESIAN_POINT ( 'NONE',  ( 2.955800887862049198, 98.65828318553602116, 5.000000000000000000 ) ) ;
#11397=UNCERTAINTY_MEASURE_WITH_UNIT (LENGTH_MEASURE( 1.000000000000000082E-05 ), #40329, 'distance_accuracy_value', 'NONE');
#11422=DIRECTION ( 'NONE',  ( -1.000000000000000000, 0.000000000000000000, 0.000000000000000000 ) ) ;
#11429=CARTESIAN_POINT ( 'NONE',  ( -10.00791540606109820, 7.488695628611232280, 0.000000000000000000 ) ) ;
#11458=CARTESIAN_POINT ( 'NONE',  ( -4.557876263184661880, 143.2026128489522989, -5.000000000000000000 ) ) ;
#11459=CARTESIAN_POINT ( 'NONE',  ( 8.986743721229322190, 136.5670193726028856, -6.141763964344532733E-13 ) ) ;
#11531=CIRCLE ( 'NONE', #6363, 5.000000000000000000 ) ;
#11621=STYLED_ITEM ( 'NONE', ( #77251 ), #43674 ) ;
#11622=CARTESIAN_POINT ( 'NONE',  ( -9.999999999999982236, 7.499999999999973355, 0.000000000000000000 ) ) ;
#11685=CARTESIAN_POINT ( 'NONE',  ( -9.061657589588678618, 137.7585088366314210, 4.999999999999998224 ) ) ;
#11705=AXIS2_PLACEMENT_3D ( 'NONE', #36644, #28020, #60369 ) ;
#11736=CARTESIAN_POINT ( 'NONE',  ( -6.221959883623910059, 4.750744965685583132, -5.000000000000037303 ) ) ;
#11791=CARTESIAN_POINT ( 'NONE',  ( 4.086538315193108950, 138.2907119265738345, 5.000000000000000000 ) ) ;
#11903=CARTESIAN_POINT ( 'NONE',  ( -8.792039765168276233, 18.71881101081278942, 0.000000000000000000 ) ) ;
#11922=ADVANCED_FACE ( 'NONE', ( #52626 ), #46657, .T. ) ;
#11972=CARTESIAN_POINT ( 'NONE',  ( -8.308397487231465206, 32.82220968432677211, -5.000000000000000000 ) ) ;
#11998=CARTESIAN_POINT ( 'NONE',  ( 7.849089830976629933, 70.34685271985473776, -5.000000000009827694 ) ) ;
#12222=CARTESIAN_POINT ( 'NONE',  ( -9.229740628973800654, 139.8534222827340159, 4.999999999999998224 ) ) ;
#12255=COLOUR_RGB ( '', 0.66274510, 0.83137255, 0.94901961) ;
#12278=CARTESIAN_POINT ( 'NONE',  ( -8.425615494702062946, 6.357254220375858189, -3.971849628822432088 ) ) ;
#12308=CIRCLE ( 'NONE', #75983, 5.000000000000000888 ) ;
#12332=CARTESIAN_POINT ( 'NONE',  ( -3.346159239404074892, 120.6791528222331777, 5.000000000000000888 ) ) ;
#12347=ORIENTED_EDGE ( 'NONE', *, *, #24440, .F. ) ;
#12363=SURFACE_STYLE_USAGE ( .BOTH. , #37214 ) ;
#12426=CARTESIAN_POINT ( 'NONE',  ( -8.241503450148531584, 35.67856248319191792, 0.000000000000000000 ) ) ;
#12466=CARTESIAN_POINT ( 'NONE',  ( 8.017333092632471292, 103.9739446863702454, 0.000000000000000000 ) ) ;
#12494=CARTESIAN_POINT ( 'NONE',  ( -9.421434414404789237, 10.25265380207672550, -8.673617380148899465E-16 ) ) ;
#12509=CARTESIAN_POINT ( 'NONE',  ( 0.000000000000000000, 152.0000000000000000, 5.000000000000000000 ) ) ;
#12521=CARTESIAN_POINT ( 'NONE',  ( -4.075111047341576587, 138.1306820922419547, -4.999999999999997335 ) ) ;
#12522=CARTESIAN_POINT ( 'NONE',  ( 2.869468778192039160, 87.32905104808958185, -5.000000000000000888 ) ) ;
#12649=COLOUR_RGB ( '', 0.66274510, 0.83137255, 0.94901961) ;
#12664=PRODUCT_DEFINITION ( 'UNKNOWN', '', #95586, #82334 ) ;
#12734=VERTEX_POINT ( 'NONE', #26044 ) ;
#12752=CARTESIAN_POINT ( 'NONE',  ( -4.504915916856424118, 9.260147447997045589, 5.000000000000000000 ) ) ;
#12805=CARTESIAN_POINT ( 'NONE',  ( -6.487288085721814035, 4.944722507271262835, -4.967589210256464050 ) ) ;
#12822=VERTEX_POINT ( 'NONE', #26563 ) ;
#12996=CARTESIAN_POINT ( 'NONE',  ( 8.216389926104845642, 36.83924058556462455, -1.301042606982605124E-15 ) ) ;
#13021=CARTESIAN_POINT ( 'NONE',  ( -8.755878939502101943, 19.75811540481800677, 6.351289142183231468E-13 ) ) ;
#13049=CARTESIAN_POINT ( 'NONE',  ( -3.742296071587391637, 132.3180728667387314, -5.000000000000000888 ) ) ;
#13050=CARTESIAN_POINT ( 'NONE',  ( 9.239881047873264919, 139.9679065713606860, 0.000000000000000000 ) ) ;
#13076=AXIS2_PLACEMENT_3D ( 'NONE', #37229, #78176, #4827 ) ;
#13243=CARTESIAN_POINT ( 'NONE',  ( 7.500000000000007105, 152.0000000000000000, -5.000000000000000000 ) ) ;
#13276=CARTESIAN_POINT ( 'NONE',  ( -8.571529135731710269, 24.05510615523603946, 1.271403623727559017E-12 ) ) ;
#13389=( GEOMETRIC_REPRESENTATION_CONTEXT ( 3 ) GLOBAL_UNCERTAINTY_ASSIGNED_CONTEXT ( ( #39822 ) ) GLOBAL_UNIT_ASSIGNED_CONTEXT ( ( #36309, #1195, #9839 ) ) REPRESENTATION_CONTEXT ( 'NONE', 'WORKASPACE' ) );
#13477=FACE_OUTER_BOUND ( 'NONE', #69069, .T. ) ;
#13539=SURFACE_SIDE_STYLE ('',( #47500 ) ) ;
#13555=CARTESIAN_POINT ( 'NONE',  ( 10.38582326156070401, 6.955909371148003117, 0.000000000000000000 ) ) ;
#13557=CARTESIAN_POINT ( 'NONE',  ( -3.241829659524363638, 35.62537785594091844, -5.000000000000000000 ) ) ;
#13579=CARTESIAN_POINT ( 'NONE',  ( 0.000000000000000000, 0.000000000000000000, 0.000000000000000000 ) ) ;
#13584=CARTESIAN_POINT ( 'NONE',  ( 7.955546711083004041, 98.60610140865000517, 0.000000000000000000 ) ) ;
#13637=FILL_AREA_STYLE ('',( #106759 ) ) ;
#13663=EDGE_LOOP ( 'NONE', ( #68138, #36181, #614, #47585 ) ) ;
#13674=CARTESIAN_POINT ( 'NONE',  ( 2.955793532184386674, 53.34242613923570531, 5.000000000000000000 ) ) ;
#13809=CARTESIAN_POINT ( 'NONE',  ( -9.316042626355404366, 11.20129626813108636, 4.999999999999999112 ) ) ;
#13811=CARTESIAN_POINT ( 'NONE',  ( -6.231493956936419387, 147.8264543773111654, 5.000000000000000000 ) ) ;
#13850=B_SPLINE_CURVE_WITH_KNOTS ( 'NONE', 3,
 ( #83345, #40231, #97932, #82818, #98457, #24085, #48834, #81724, #73646, #33761, #7851, #788, #41823, #57998, #25140, #58556, #40756, #260, #32703, #106550, #66633, #99518 ),
 .UNSPECIFIED., .F., .F.,
 ( 4, 2, 2, 2, 2, 2, 2, 2, 2, 2, 4 ),
 ( 2.469733450048283490E-18, 0.0009764592657812548029, 0.001464688898671880849, 0.001952918531562507004, 0.002929377797343762132, 0.003905837063125017043, 0.004882296328906272388, 0.005858755594687526866, 0.006835214860468781344, 0.007323444493359409016, 0.007811674126250036689 ),
 .UNSPECIFIED. ) ;
#13853=CARTESIAN_POINT ( 'NONE',  ( 3.443305032968370760, 124.1406189207604172, -4.999999999999999112 ) ) ;
#13911=EDGE_CURVE ( 'NONE', #105180, #76218, #37344, .T. ) ;
#13951=( NAMED_UNIT ( * ) SI_UNIT ( $, .STERADIAN. ) SOLID_ANGLE_UNIT ( ) );
#13964=CIRCLE ( 'NONE', #74266, 5.000000000000001776 ) ;
#14058=CARTESIAN_POINT ( 'NONE',  ( 9.209506619794041171, 139.6161984561731799, -1.301042606982606899E-15 ) ) ;
#14065=DIRECTION ( 'NONE',  ( 0.000000000000000000, 0.000000000000000000, -1.000000000000000000 ) ) ;
#14082=CARTESIAN_POINT ( 'NONE',  ( -4.857429444120077378, 7.134197903804992080, -5.000000000000000000 ) ) ;
#14096=FACE_OUTER_BOUND ( 'NONE', #75947, .T. ) ;
#14113=CARTESIAN_POINT ( 'NONE',  ( 8.224467148746322565, 36.45870262746143453, -4.999999999999998224 ) ) ;
#14173=PRESENTATION_STYLE_ASSIGNMENT (( #47606 ) ) ;
#14333=CARTESIAN_POINT ( 'NONE',  ( -4.866346026169152239, 7.094448090634657866, 5.000000000000000000 ) ) ;
#14410=STYLED_ITEM ( 'NONE', ( #46970 ), #17821 ) ;
#14438=CARTESIAN_POINT ( 'NONE',  ( 4.561387878963821585, 143.2234794286142403, 5.000000000000000000 ) ) ;
#14444=CARTESIAN_POINT ( 'NONE',  ( -2.854624676502999669, 68.28528602110660017, 4.999999999999998224 ) ) ;
#14470=FACE_OUTER_BOUND ( 'NONE', #38626, .T. ) ;
#14500=ADVANCED_FACE ( 'NONE', ( #24491 ), #82961, .T. ) ;
#14514=DIRECTION ( 'NONE',  ( -0.8308658609248562588, -0.5564727496918402405, 0.000000000000000000 ) ) ;
#14590=FACE_OUTER_BOUND ( 'NONE', #51249, .T. ) ;
#14599=MECHANICAL_DESIGN_GEOMETRIC_PRESENTATION_REPRESENTATION('',(#790),#50788);
#14639=CARTESIAN_POINT ( 'NONE',  ( 7.869432500667118191, 64.69453614009768216, -2.456524630699382222E-12 ) ) ;
#14673=( GEOMETRIC_REPRESENTATION_CONTEXT ( 3 ) GLOBAL_UNCERTAINTY_ASSIGNED_CONTEXT ( ( #42686 ) ) GLOBAL_UNIT_ASSIGNED_CONTEXT ( ( #58899, #34115, #66986 ) ) REPRESENTATION_CONTEXT ( 'NONE', 'WORKASPACE' ) );
#14705=CARTESIAN_POINT ( 'NONE',  ( 9.075061004355044147, 14.05394893828536063, -6.138968940038654494E-13 ) ) ;
#14716=ADVANCED_FACE ( 'NONE', ( #93311 ), #33838, .T. ) ;
#14869=CARTESIAN_POINT ( 'NONE',  ( -5.863284779130247593, 4.691109759206348429, 4.999999999999999112 ) ) ;
#14926=CARTESIAN_POINT ( 'NONE',  ( -9.172731267813459155, 6.899963662535627762, -3.046434832396871961 ) ) ;
#14980=( NAMED_UNIT ( * ) SI_UNIT ( $, .STERADIAN. ) SOLID_ANGLE_UNIT ( ) );
#14983=CARTESIAN_POINT ( 'NONE',  ( 0.000000000000000000, 0.000000000000000000, 0.000000000000000000 ) ) ;
#14993=CIRCLE ( 'NONE', #66750, 4.999999999999999112 ) ;
#15030=EDGE_CURVE ( 'NONE', #84815, #10145, #47646, .T. ) ;
#15155=CARTESIAN_POINT ( 'NONE',  ( -3.342518420180325300, 120.5426393934660609, -4.999999999999999112 ) ) ;
#15183=CARTESIAN_POINT ( 'NONE',  ( 8.167412539202029365, 39.27912669871973605, -5.000000000000000888 ) ) ;
#15203=CARTESIAN_POINT ( 'NONE',  ( -7.500000000000000888, 0.000000000000000000, 0.000000000000000000 ) ) ;
#15249=CARTESIAN_POINT ( 'NONE',  ( 3.996239228619476336, 15.12369778636299777, 4.999999999999999112 ) ) ;
#15260=COLOUR_RGB ( '', 0.08235294, 0.09019608, 0.10196078) ;
#15276=CARTESIAN_POINT ( 'NONE',  ( 4.258999010316452782, 140.4059127768352653, 5.000000000000000000 ) ) ;
#15346=AXIS2_PLACEMENT_3D ( 'NONE', #2246, #52943, #2791 ) ;
#15406=FACE_OUTER_BOUND ( 'NONE', #57825, .T. ) ;
#15407=CARTESIAN_POINT ( 'NONE',  ( -10.31642403553700937, 7.048099644362468830, 0.000000000000000000 ) ) ;
#15519=ORIENTED_EDGE ( 'NONE', *, *, #38703, .F. ) ;
#15532=DIRECTION ( 'NONE',  ( -1.000000000000000000, 0.000000000000000000, 0.000000000000000000 ) ) ;
#15715=STYLED_ITEM ( 'NONE', ( #95969 ), #79708 ) ;
#15718=CARTESIAN_POINT ( 'NONE',  ( 3.591939471458723609, 23.61027659479541896, -5.000000000000000000 ) ) ;
#15735=CARTESIAN_POINT ( 'NONE',  ( -5.000000000000002665, 152.0000000000000000, 5.000000000000000000 ) ) ;
#15780=CARTESIAN_POINT ( 'NONE',  ( 8.830611806799852914, 18.20472706776858018, 6.133090346964878919E-13 ) ) ;
#15805=CARTESIAN_POINT ( 'NONE',  ( 3.225563553360615288, 115.6469223491950515, 5.000000000000000000 ) ) ;
#15826=CIRCLE ( 'NONE', #27902, 5.000000000000000000 ) ;
#15851=DIRECTION ( 'NONE',  ( -1.000000000000000000, 0.000000000000000000, 0.000000000000000000 ) ) ;
#15870=CARTESIAN_POINT ( 'NONE',  ( 12.50000000000000533, 152.0000000000000000, 0.000000000000000000 ) ) ;
#15942=CARTESIAN_POINT ( 'NONE',  ( -10.41860328468676755, 6.902172553357436513, 4.999999999999923617 ) ) ;
#16000=PLANE ( 'NONE',  #54322 ) ;
#16004=CARTESIAN_POINT ( 'NONE',  ( -9.001979478496508591, 6.776006056211794082, -3.303702010581815784 ) ) ;
#16068=EDGE_LOOP ( 'NONE', ( #64969, #88370 ) ) ;
#16070=EDGE_CURVE ( 'NONE', #1254, #10915, #101173, .T. ) ;
#16119=CARTESIAN_POINT ( 'NONE',  ( 0.000000000000000000, 152.0000000000000000, 5.000000000000000000 ) ) ;
#16214=CARTESIAN_POINT ( 'NONE',  ( -9.230092720259007066, 139.8575112583662019, -5.000000000000000888 ) ) ;
#16236=MECHANICAL_DESIGN_GEOMETRIC_PRESENTATION_REPRESENTATION('',(#4106),#85164);
#16247=CARTESIAN_POINT ( 'NONE',  ( 4.474875413804290325, 9.478657632136659572, -5.000000000000000000 ) ) ;
#16312=AXIS2_PLACEMENT_3D ( 'NONE', #22772, #88547, #55609 ) ;
#16476=CARTESIAN_POINT ( 'NONE',  ( -5.952443285071600698, 4.563276076495102807, 4.999999999999999112 ) ) ;
#16527=DIRECTION ( 'NONE',  ( 0.000000000000000000, 0.000000000000000000, -1.000000000000000000 ) ) ;
#16530=CIRCLE ( 'NONE', #80266, 5.000000000000002665 ) ;
#16603=CARTESIAN_POINT ( 'NONE',  ( -9.291504854928620105, 140.5441818689093054, 5.000000000000954792 ) ) ;
#16658=DIRECTION ( 'NONE',  ( -1.000000000000000000, 0.000000000000000000, 0.000000000000000000 ) ) ;
#16753=CARTESIAN_POINT ( 'NONE',  ( -2.860373741371127654, 85.40625066822151723, -5.000000000000002665 ) ) ;
#16836=CARTESIAN_POINT ( 'NONE',  ( -5.956988534971662475, 4.556784786910193397, 5.000000000000000000 ) ) ;
#16857=CARTESIAN_POINT ( 'NONE',  ( 7.869432500667418395, 87.30546385994318825, 0.000000000000000000 ) ) ;
#16859=TOROIDAL_SURFACE ( 'NONE', #58177, 7.500000000000000888, 5.000000000000000000 ) ;
#16928=CARTESIAN_POINT ( 'NONE',  ( -4.640293713146470544, 8.300177736797209604, -5.000000000000000000 ) ) ;
#16930=AXIS2_PLACEMENT_3D ( 'NONE', #38800, #54952, #104576 ) ;
#17020=CARTESIAN_POINT ( 'NONE',  ( -10.11206553723567936, 7.339953826372402013, 5.000000000000038192 ) ) ;
#17305=SURFACE_STYLE_USAGE ( .BOTH. , #91197 ) ;
#17380=FILL_AREA_STYLE ('',( #18448 ) ) ;
#17632=CIRCLE ( 'NONE', #84828, 5.000000000000000888 ) ;
#17633=PRESENTATION_STYLE_ASSIGNMENT (( #18166 ) ) ;
#17644=DIRECTION ( 'NONE',  ( 0.9861333108788017388, 0.1659550938513567886, 0.000000000000000000 ) ) ;
#17726=ORIENTED_EDGE ( 'NONE', *, *, #9891, .T. ) ;
#17756=SURFACE_SIDE_STYLE ('',( #93231 ) ) ;
#17821=ADVANCED_FACE ( 'NONE', ( #14590 ), #100577, .T. ) ;
#17829=ORIENTED_EDGE ( 'NONE', *, *, #3881, .F. ) ;
#17837=( LENGTH_UNIT ( ) NAMED_UNIT ( * ) SI_UNIT ( .MILLI., .METRE. ) );
#17961=ORIENTED_EDGE ( 'NONE', *, *, #26824, .F. ) ;
#17965=CARTESIAN_POINT ( 'NONE',  ( -10.01459525654356852, 7.479155813459360758, 0.000000000000000000 ) ) ;
#18064=VERTEX_POINT ( 'NONE', #87854 ) ;
#18166=SURFACE_STYLE_USAGE ( .BOTH. , #91517 ) ;
#18222=CARTESIAN_POINT ( 'NONE',  ( -8.067121135846440083, 44.45135178119163299, 0.000000000000000000 ) ) ;
#18299=FACE_OUTER_BOUND ( 'NONE', #71906, .T. ) ;
#18448=FILL_AREA_STYLE_COLOUR ( '', #62914 ) ;
#18481=DIRECTION ( 'NONE',  ( 0.1659550938513567053, -0.9861333108788017388, 0.000000000000000000 ) ) ;
#18504=CARTESIAN_POINT ( 'NONE',  ( -5.859023161960823955, 4.697346715784889604, -4.999999999999999112 ) ) ;
#18752=DIRECTION ( 'NONE',  ( -1.000000000000000000, 0.000000000000000000, 0.000000000000000000 ) ) ;
#18753=CARTESIAN_POINT ( 'NONE',  ( 0.000000000000000000, 152.0000000000000000, -5.000000000000000000 ) ) ;
#18773=CARTESIAN_POINT ( 'NONE',  ( -2.883864260984685401, 61.94980599433312562, 5.000000000000000000 ) ) ;
#18879=CARTESIAN_POINT ( 'NONE',  ( 2.849089834145952516, 81.66538534281866646, 5.000000000000000000 ) ) ;
#19055=CARTESIAN_POINT ( 'NONE',  ( -6.232788007775230454, 4.162902319565254139, -5.000000000000000000 ) ) ;
#19117=ADVANCED_FACE ( 'NONE', ( #20027 ), #75938, .T. ) ;
#19175=MECHANICAL_DESIGN_GEOMETRIC_PRESENTATION_REPRESENTATION('',(#15715),#26098);
#19177=STYLED_ITEM ( 'NONE', ( #4322 ), #19117 ) ;
#19324=CARTESIAN_POINT ( 'NONE',  ( -2.844355883296552090, 79.52658463821998680, 5.000000000000000000 ) ) ;
#19421=CARTESIAN_POINT ( 'NONE',  ( 2.869473476665008516, 87.32989181417194402, 5.000000000000000000 ) ) ;
#19595=CARTESIAN_POINT ( 'NONE',  ( -10.16823181764058859, 7.259740064965935602, 0.000000000000000000 ) ) ;
#19624=CARTESIAN_POINT ( 'NONE',  ( 4.322723262674379896, 141.1105290361839479, -4.999999999999999112 ) ) ;
#19643=MECHANICAL_DESIGN_GEOMETRIC_PRESENTATION_REPRESENTATION('',(#14410),#95422);
#19705=CARTESIAN_POINT ( 'NONE',  ( 0.000000000000000000, 0.000000000000000000, 0.000000000000000000 ) ) ;
#19846=CARTESIAN_POINT ( 'NONE',  ( -7.856156674180255983, 67.82625813595271325, 5.000000000000000000 ) ) ;
#19907=DIRECTION ( 'NONE',  ( 0.000000000000000000, 0.000000000000000000, -1.000000000000000000 ) ) ;
#19952=CARTESIAN_POINT ( 'NONE',  ( 8.986804597164578468, 136.5680015418715811, 8.673617379999392574E-16 ) ) ;
#20027=FACE_OUTER_BOUND ( 'NONE', #25986, .T. ) ;
#20054=CARTESIAN_POINT ( 'NONE',  ( -7.865987974594087717, 86.57916236585580805, 1.301042606982605124E-15 ) ) ;
#20079=MECHANICAL_DESIGN_GEOMETRIC_PRESENTATION_REPRESENTATION('',(#76838),#38976);
#20123=CARTESIAN_POINT ( 'NONE',  ( -3.830996925285758525, 18.06395145735098140, -5.000000000000000000 ) ) ;
#20135=UNCERTAINTY_MEASURE_WITH_UNIT (LENGTH_MEASURE( 1.000000000000000082E-05 ), #62164, 'distance_accuracy_value', 'NONE');
#20146=AXIS2_PLACEMENT_3D ( 'NONE', #47137, #95185, #87094 ) ;
#20153=CARTESIAN_POINT ( 'NONE',  ( -3.625560833898588964, 129.4090813058823812, -5.000000000000000888 ) ) ;
#20154=CARTESIAN_POINT ( 'NONE',  ( 3.225593670032574689, 115.6483099733404458, -5.000000000000000000 ) ) ;
#20156=DIRECTION ( 'NONE',  ( -1.000000000000000000, -1.224646799147353207E-16, 0.000000000000000000 ) ) ;
#20243=CARTESIAN_POINT ( 'NONE',  ( 3.757221660946450825, 19.36720549871765940, 4.999999999999998224 ) ) ;
#20390=CARTESIAN_POINT ( 'NONE',  ( -7.989648714934757479, 50.29308867530622251, 5.000000000000000888 ) ) ;
#20473=ORIENTED_EDGE ( 'NONE', *, *, #55290, .F. ) ;
#20519=EDGE_LOOP ( 'NONE', ( #46549, #22760, #52869, #25629 ) ) ;
#20596=FACE_BOUND ( 'NONE', #88468, .T. ) ;
#20603=CARTESIAN_POINT ( 'NONE',  ( -9.491976138786448303, 142.3932387565501472, 0.000000000000000000 ) ) ;
#20617=COLOUR_RGB ( '', 0.72549020, 0.75294118, 0.79215686) ;
#20638=AXIS2_PLACEMENT_3D ( 'NONE', #4884, #61011, #38335 ) ;
#20668=CARTESIAN_POINT ( 'NONE',  ( -7.989277284024328019, 50.32447066042715988, 0.000000000000000000 ) ) ;
#20696=CARTESIAN_POINT ( 'NONE',  ( 9.239881048100823335, 139.9679065713421267, -5.000000000000000888 ) ) ;
#20919=CARTESIAN_POINT ( 'NONE',  ( -9.998846395913654206, 7.501654003228592771, 5.000000000000001776 ) ) ;
#21017=CARTESIAN_POINT ( 'NONE',  ( -4.469491342313713922, 142.4783567884534818, 5.000000000000000000 ) ) ;
#21156=CARTESIAN_POINT ( 'NONE',  ( 9.609486011791450011, 8.908497650347621644, 0.000000000000000000 ) ) ;
#21181=CARTESIAN_POINT ( 'NONE',  ( -9.311676254474896552, 11.24588917688063106, -8.673617379354307486E-16 ) ) ;
#21189=( NAMED_UNIT ( * ) SI_UNIT ( $, .STERADIAN. ) SOLID_ANGLE_UNIT ( ) );
#21205=CARTESIAN_POINT ( 'NONE',  ( -4.469712646659624866, 142.4802100387212533, -5.000000000000000000 ) ) ;
#21369=( NAMED_UNIT ( * ) PLANE_ANGLE_UNIT ( ) SI_UNIT ( $, .RADIAN. ) );
#21417=CARTESIAN_POINT ( 'NONE',  ( -9.743481591712932044, 8.211523606034065281, 0.000000000000000000 ) ) ;
#21430=FACE_OUTER_BOUND ( 'NONE', #51220, .T. ) ;
#21529=CARTESIAN_POINT ( 'NONE',  ( -2.861889033126343573, 85.75214027433212038, 4.999999999999998224 ) ) ;
#21565=FILL_AREA_STYLE_COLOUR ( '', #12255 ) ;
#21600=DIRECTION ( 'NONE',  ( 0.000000000000000000, 0.000000000000000000, -1.000000000000000000 ) ) ;
#21625=( NAMED_UNIT ( * ) PLANE_ANGLE_UNIT ( ) SI_UNIT ( $, .RADIAN. ) );
#21627=CARTESIAN_POINT ( 'NONE',  ( -8.031083489010908849, 46.98771334398849575, 0.000000000000000000 ) ) ;
#21673=CARTESIAN_POINT ( 'NONE',  ( 9.046057234714689699, 137.5248812442146971, -1.301042606982603940E-15 ) ) ;
#21699=CARTESIAN_POINT ( 'NONE',  ( -5.435697248882358501, 5.410530404478980593, -4.999999999999999112 ) ) ;
#21726=CARTESIAN_POINT ( 'NONE',  ( 8.441095186759753233, 123.9902009031629717, -5.000000000000000000 ) ) ;
#21913=DIRECTION ( 'NONE',  ( -0.000000000000000000, -0.000000000000000000, 1.000000000000000000 ) ) ;
#21947=CARTESIAN_POINT ( 'NONE',  ( -9.465790868195963270, 9.886732697601933850, 5.000000000000158984 ) ) ;
#21984=( NAMED_UNIT ( * ) SI_UNIT ( $, .STERADIAN. ) SOLID_ANGLE_UNIT ( ) );
#21989=FACE_OUTER_BOUND ( 'NONE', #45129, .T. ) ;
#22042=AXIS2_PLACEMENT_3D ( 'NONE', #101756, #37061, #18752 ) ;
#22051=DIRECTION ( 'NONE',  ( -1.000000000000000000, 0.000000000000000000, 0.000000000000000000 ) ) ;
#22083=( NAMED_UNIT ( * ) PLANE_ANGLE_UNIT ( ) SI_UNIT ( $, .RADIAN. ) );
#22197=CARTESIAN_POINT ( 'NONE',  ( 8.216398312217762623, 115.1611316811069798, 0.000000000000000000 ) ) ;
#22212=EDGE_CURVE ( 'NONE', #53832, #84815, #74885, .T. ) ;
#22226=CARTESIAN_POINT ( 'NONE',  ( -9.311676253867856801, 11.24588917681355049, -5.000000000000000000 ) ) ;
#22239=DIRECTION ( 'NONE',  ( -1.000000000000000000, 0.000000000000000000, 0.000000000000000000 ) ) ;
#22254=CARTESIAN_POINT ( 'NONE',  ( 8.986804597165106046, 15.43199845811895266, 9.201869806248672558E-30 ) ) ;
#22294=ORIENTED_EDGE ( 'NONE', *, *, #59211, .F. ) ;
#22319=CARTESIAN_POINT ( 'NONE',  ( 9.300358455352606413, 11.36566808881823754, 4.999999999998467004 ) ) ;
#22340=ORIENTED_EDGE ( 'NONE', *, *, #35706, .T. ) ;
#22429=UNCERTAINTY_MEASURE_WITH_UNIT (LENGTH_MEASURE( 1.000000000000000082E-05 ), #52356, 'distance_accuracy_value', 'NONE');
#22436=DIRECTION ( 'NONE',  ( -0.000000000000000000, -0.000000000000000000, 1.000000000000000000 ) ) ;
#22486=CARTESIAN_POINT ( 'NONE',  ( -9.079631412095446663, 13.97901777655708067, 4.999999999999364064 ) ) ;
#22530=SURFACE_STYLE_USAGE ( .BOTH. , #96399 ) ;
#22598=CARTESIAN_POINT ( 'NONE',  ( -2.942711189959360762, 97.39608628791339129, 5.000000000000000000 ) ) ;
#22637=( NAMED_UNIT ( * ) PLANE_ANGLE_UNIT ( ) SI_UNIT ( $, .RADIAN. ) );
#22731=CARTESIAN_POINT ( 'NONE',  ( 8.959983754892499874, 15.87132973532702174, -2.602085213965211825E-15 ) ) ;
#22757=CARTESIAN_POINT ( 'NONE',  ( -8.972157809163535447, 136.3338258388613440, -5.000000000000003553 ) ) ;
#22760=ORIENTED_EDGE ( 'NONE', *, *, #88763, .F. ) ;
#22772=CARTESIAN_POINT ( 'NONE',  ( 0.000000000000000000, 0.000000000000000000, 5.000000000000000000 ) ) ;
#22785=CARTESIAN_POINT ( 'NONE',  ( 8.441132293727447333, 28.00851920974784548, -5.000000000001228351 ) ) ;
#22848=CARTESIAN_POINT ( 'NONE',  ( 8.986743721356470260, 15.43298062744866961, 4.999999999999999112 ) ) ;
#22882=SHAPE_DEFINITION_REPRESENTATION ( #4568, #70207 ) ;
#22954=PRESENTATION_STYLE_ASSIGNMENT (( #96825 ) ) ;
#22962=CARTESIAN_POINT ( 'NONE',  ( 7.500000000000000888, 9.184850993605149917E-16, 0.000000000000000000 ) ) ;
#22967=ORIENTED_EDGE ( 'NONE', *, *, #2710, .T. ) ;
#23004=CARTESIAN_POINT ( 'NONE',  ( -9.596328385228648727, 8.973060046565024095, 0.000000000000000000 ) ) ;
#23016=MECHANICAL_DESIGN_GEOMETRIC_PRESENTATION_REPRESENTATION('',(#64270),#40156);
#23280=CARTESIAN_POINT ( 'NONE',  ( -4.072841793016302780, 138.0987898825082709, -5.000000000000000000 ) ) ;
#23309=CARTESIAN_POINT ( 'NONE',  ( 4.323075853814730252, 10.88581780261195142, -5.000000000000000000 ) ) ;
#23372=CARTESIAN_POINT ( 'NONE',  ( 4.678819457397437098, 8.078722181090839172, 5.000000000000000000 ) ) ;
#23374=DIRECTION ( 'NONE',  ( 0.5564727496918392413, -0.8308658609248569249, 1.930652685263598448E-16 ) ) ;
#23490=ORIENTED_EDGE ( 'NONE', *, *, #92450, .T. ) ;
#23537=CARTESIAN_POINT ( 'NONE',  ( -10.03543110037283093, 7.449399144625810543, 5.000000000000000888 ) ) ;
#23582=CARTESIAN_POINT ( 'NONE',  ( 4.086350204929699359, 138.2877876407195004, -5.000000000000000888 ) ) ;
#23583=( NAMED_UNIT ( * ) PLANE_ANGLE_UNIT ( ) SI_UNIT ( $, .RADIAN. ) );
#23648=UNCERTAINTY_MEASURE_WITH_UNIT (LENGTH_MEASURE( 1.000000000000000082E-05 ), #10926, 'distance_accuracy_value', 'NONE');
#23662=CARTESIAN_POINT ( 'NONE',  ( -4.556959930218859256, 143.1971678044430405, 5.000000000000004441 ) ) ;
#23825=CARTESIAN_POINT ( 'NONE',  ( -9.609486011791425142, 143.0915023496523020, 0.000000000000000000 ) ) ;
#23842=CIRCLE ( 'NONE', #34159, 5.000000000000000888 ) ;
#23852=CARTESIAN_POINT ( 'NONE',  ( 9.609486011791085858, 8.908497650349776364, -5.000000000000000888 ) ) ;
#23914=SURFACE_STYLE_FILL_AREA ( #71891 ) ;
#23926=ORIENTED_EDGE ( 'NONE', *, *, #23994, .F. ) ;
#23994=EDGE_CURVE ( 'NONE', #39330, #53832, #11531, .T. ) ;
#24070=CARTESIAN_POINT ( 'NONE',  ( -6.016305315790704711, 4.472071644617155783, 4.999999999999999112 ) ) ;
#24085=CARTESIAN_POINT ( 'NONE',  ( -9.787706584712674740, 7.346100692761604378, 1.606208808826772749 ) ) ;
#24086=AXIS2_PLACEMENT_3D ( 'NONE', #62345, #87148, #90311 ) ;
#24114=ORIENTED_EDGE ( 'NONE', *, *, #41556, .F. ) ;
#24133=CARTESIAN_POINT ( 'NONE',  ( -8.629057352428841199, 6.505111962821877647, -3.764883966312650987 ) ) ;
#24173=( GEOMETRIC_REPRESENTATION_CONTEXT ( 3 ) GLOBAL_UNCERTAINTY_ASSIGNED_CONTEXT ( ( #49412 ) ) GLOBAL_UNIT_ASSIGNED_CONTEXT ( ( #95760, #21369, #63413 ) ) REPRESENTATION_CONTEXT ( 'NONE', 'WORKASPACE' ) );
#24185=DIRECTION ( 'NONE',  ( 0.000000000000000000, 0.000000000000000000, -1.000000000000000000 ) ) ;
#24193=CIRCLE ( 'NONE', #70662, 7.500000000000006217 ) ;
#24282=( GEOMETRIC_REPRESENTATION_CONTEXT ( 3 ) GLOBAL_UNCERTAINTY_ASSIGNED_CONTEXT ( ( #86883 ) ) GLOBAL_UNIT_ASSIGNED_CONTEXT ( ( #92032, #96306, #102253 ) ) REPRESENTATION_CONTEXT ( 'NONE', 'WORKASPACE' ) );
#24323=VERTEX_POINT ( 'NONE', #55036 ) ;
#24350=CARTESIAN_POINT ( 'NONE',  ( -3.739146603194685614, 132.2511161815098149, -5.000000000000002665 ) ) ;
#24384=CARTESIAN_POINT ( 'NONE',  ( 3.996301576407919498, 15.12269148464774737, -5.000000000000000000 ) ) ;
#24440=EDGE_CURVE ( 'NONE', #83314, #80759, #14993, .T. ) ;
#24450=( NAMED_UNIT ( * ) PLANE_ANGLE_UNIT ( ) SI_UNIT ( $, .RADIAN. ) );
#24491=FACE_OUTER_BOUND ( 'NONE', #77077, .T. ) ;
#24595=CARTESIAN_POINT ( 'NONE',  ( -10.16315516181093592, 7.266990280869982222, 5.000000000000000888 ) ) ;
#24643=CARTESIAN_POINT ( 'NONE',  ( 4.474623633716955595, 9.480714495128564678, -4.999999999999998224 ) ) ;
#24814=( LENGTH_UNIT ( ) NAMED_UNIT ( * ) SI_UNIT ( .MILLI., .METRE. ) );
#24852=AXIS2_PLACEMENT_3D ( 'NONE', #46705, #79601, #53217 ) ;
#24866=CARTESIAN_POINT ( 'NONE',  ( -3.622206768987289660, 129.3245652911131174, -4.999999999999999112 ) ) ;
#24963=CARTESIAN_POINT ( 'NONE',  ( 8.642300018659518912, 129.6053270932845294, 5.000000000000000888 ) ) ;
#25004=FILL_AREA_STYLE ('',( #90247 ) ) ;
#25033=AXIS2_PLACEMENT_3D ( 'NONE', #43508, #92050, #25777 ) ;
#25125=CARTESIAN_POINT ( 'NONE',  ( -9.999586304451581142, 7.500591597932315224, 0.000000000000000000 ) ) ;
#25140=CARTESIAN_POINT ( 'NONE',  ( -7.748578893116479627, 5.864678312211424327, 4.493043914853660503 ) ) ;
#25245=PRESENTATION_STYLE_ASSIGNMENT (( #66198 ) ) ;
#25419=STYLED_ITEM ( 'NONE', ( #27316 ), #26428 ) ;
#25442=ORIENTED_EDGE ( 'NONE', *, *, #6526, .F. ) ;
#25536=SHAPE_REPRESENTATION_RELATIONSHIP ( 'NONE' , 'NONE' ,  #70207, #51084 ) ;
#25629=ORIENTED_EDGE ( 'NONE', *, *, #49192, .T. ) ;
#25690=CARTESIAN_POINT ( 'NONE',  ( 6.231493956936422940, 4.173545622688802581, 0.000000000000000000 ) ) ;
#25731=CARTESIAN_POINT ( 'NONE',  ( 3.168296453696544557, 39.18458251124699387, -5.000000000000000000 ) ) ;
#25758=FILL_AREA_STYLE ('',( #99581 ) ) ;
#25777=DIRECTION ( 'NONE',  ( 1.000000000000000000, 0.000000000000000000, 0.000000000000000000 ) ) ;
#25880=COLOUR_RGB ( '', 0.72549020, 0.75294118, 0.79215686) ;
#25888=ORIENTED_EDGE ( 'NONE', *, *, #15030, .T. ) ;
#25965=SURFACE_STYLE_FILL_AREA ( #521 ) ;
#25972=CARTESIAN_POINT ( 'NONE',  ( 14.54015256618498775, 9.738273119607207207, -5.000000000000000000 ) ) ;
#25986=EDGE_LOOP ( 'NONE', ( #98822, #79790, #5848, #23926 ) ) ;
#26040=SURFACE_STYLE_USAGE ( .BOTH. , #83155 ) ;
#26044=CARTESIAN_POINT ( 'NONE',  ( 6.231493956936422940, 4.173545622688802581, -5.000000000000000000 ) ) ;
#26053=CIRCLE ( 'NONE', #100054, 5.000000000000000888 ) ;
#26094=CARTESIAN_POINT ( 'NONE',  ( -9.999565592957996074, 7.500620397551100993, 0.000000000000000000 ) ) ;
#26098=( GEOMETRIC_REPRESENTATION_CONTEXT ( 3 ) GLOBAL_UNCERTAINTY_ASSIGNED_CONTEXT ( ( #10047 ) ) GLOBAL_UNIT_ASSIGNED_CONTEXT ( ( #87876, #22637, #62540 ) ) REPRESENTATION_CONTEXT ( 'NONE', 'WORKASPACE' ) );
#26123=CARTESIAN_POINT ( 'NONE',  ( -4.201140726046737939, 12.27787011423575692, -5.000000000000000000 ) ) ;
#26136=ORIENTED_EDGE ( 'NONE', *, *, #82201, .F. ) ;
#26288=CIRCLE ( 'NONE', #53791, 9.999999999999998224 ) ;
#26343=CARTESIAN_POINT ( 'NONE',  ( -8.002549191641280757, 102.8991202088222252, 2.540710531356172437E-12 ) ) ;
#26349=STYLED_ITEM ( 'NONE', ( #99095 ), #96183 ) ;
#26428=ADVANCED_FACE ( 'NONE', ( #101154 ), #16859, .T. ) ;
#26459=ORIENTED_EDGE ( 'NONE', *, *, #82052, .T. ) ;
#26563=CARTESIAN_POINT ( 'NONE',  ( 4.678819457397437986, 8.078722181090837395, -5.000000000000000000 ) ) ;
#26615=CARTESIAN_POINT ( 'NONE',  ( -9.943426268670526369, 7.591391548649984777, 0.000000000000000000 ) ) ;
#26787=CARTESIAN_POINT ( 'NONE',  ( 4.678819457397437986, 8.078722181090837395, -5.000000000000000000 ) ) ;
#26824=EDGE_CURVE ( 'NONE', #10145, #44815, #104765, .T. ) ;
#26867=CARTESIAN_POINT ( 'NONE',  ( -7.856156674185535316, 67.82625813595271325, 0.000000000000000000 ) ) ;
#26952=ORIENTED_EDGE ( 'NONE', *, *, #38703, .T. ) ;
#26964=CARTESIAN_POINT ( 'NONE',  ( 7.955546711082998712, 53.39389859135090433, 2.456618345357718155E-12 ) ) ;
#27146=CARTESIAN_POINT ( 'NONE',  ( -6.019032792335750948, 4.468176404425925341, -5.000000000000000000 ) ) ;
#27169=CARTESIAN_POINT ( 'NONE',  ( -4.839353126352284207, 7.222265015501570851, -5.000000000000000000 ) ) ;
#27303=DIRECTION ( 'NONE',  ( -1.000000000000000000, 0.000000000000000000, 0.000000000000000000 ) ) ;
#27316=PRESENTATION_STYLE_ASSIGNMENT (( #50458 ) ) ;
#27409=CARTESIAN_POINT ( 'NONE',  ( -8.623093486195200441, 129.1228760232908144, 4.999999999999366729 ) ) ;
#27461=CARTESIAN_POINT ( 'NONE',  ( 7.500000000000000888, 1.224646799147353256E-15, -5.000000000000000000 ) ) ;
#27507=CARTESIAN_POINT ( 'NONE',  ( 8.642300018713374499, 129.6053270932821135, -6.133294652287071463E-13 ) ) ;
#27555=CIRCLE ( 'NONE', #44854, 12.50000000000000000 ) ;
#27684=CARTESIAN_POINT ( 'NONE',  ( -5.918835035098597430, 4.611273631704160714, -4.999999999999999112 ) ) ;
#27710=CARTESIAN_POINT ( 'NONE',  ( -2.861896996888536382, 85.75376362043782308, -5.000000000000000000 ) ) ;
#27811=DIRECTION ( 'NONE',  ( -1.000000000000000000, 0.000000000000000000, 0.000000000000000000 ) ) ;
#27902=AXIS2_PLACEMENT_3D ( 'NONE', #104732, #61108, #20156 ) ;
#27939=CARTESIAN_POINT ( 'NONE',  ( -3.204808325454104878, 114.6770343510770402, 5.000000000000000000 ) ) ;
#28020=DIRECTION ( 'NONE',  ( -0.000000000000000000, -0.000000000000000000, 1.000000000000000000 ) ) ;
#28034=CARTESIAN_POINT ( 'NONE',  ( 8.224467148743913825, 115.5412973725997716, 4.999999999998771649 ) ) ;
#28052=EDGE_CURVE ( 'NONE', #97405, #1352, #4848, .T. ) ;
#28136=CARTESIAN_POINT ( 'NONE',  ( -8.343637927466835080, 120.5097608953729775, 1.301042606982606110E-15 ) ) ;
#28211=CARTESIAN_POINT ( 'NONE',  ( -2.989615061350497260, 50.26451032649107020, -4.999999999999999112 ) ) ;
#28234=CARTESIAN_POINT ( 'NONE',  ( 8.986743721355239245, 136.5670193725957233, -5.000000000000612843 ) ) ;
#28313=CARTESIAN_POINT ( 'NONE',  ( 4.678819457397437986, 8.078722181090837395, 5.000000000000000000 ) ) ;
#28456=CARTESIAN_POINT ( 'NONE',  ( -7.989648714920444483, 50.29308867528581573, 0.000000000000000000 ) ) ;
#28557=CARTESIAN_POINT ( 'NONE',  ( 3.021271035815610073, 47.67815885094228179, 5.000000000000000000 ) ) ;
#28658=DIRECTION ( 'NONE',  ( -1.000000000000000000, 0.000000000000000000, -0.000000000000000000 ) ) ;
#28685=COLOUR_RGB ( '', 0.31764706, 0.68627451, 0.89019608) ;
#28707=ORIENTED_EDGE ( 'NONE', *, *, #5792, .T. ) ;
#28724=DIRECTION ( 'NONE',  ( 0.8308658609248538163, -0.5564727496918439043, -1.776356839400249479E-15 ) ) ;
#28739=CARTESIAN_POINT ( 'NONE',  ( -8.824767335865399076, 18.31512251394013191, 0.000000000000000000 ) ) ;
#28775=CARTESIAN_POINT ( 'NONE',  ( 4.258978623648461692, 140.4056380026280237, -5.000000000000000000 ) ) ;
#28847=ORIENTED_EDGE ( 'NONE', *, *, #58259, .F. ) ;
#28971=DIRECTION ( 'NONE',  ( -1.000000000000000000, 0.000000000000000000, 0.000000000000000000 ) ) ;
#29011=CARTESIAN_POINT ( 'NONE',  ( -9.465790868675496128, 9.886732697667790504, 0.000000000000000000 ) ) ;
#29053=EDGE_LOOP ( 'NONE', ( #78466, #79266, #22340, #17961 ) ) ;
#29117=CARTESIAN_POINT ( 'NONE',  ( -3.293777686966706142, 33.35761369607794791, 5.000000000000000888 ) ) ;
#29189=CARTESIAN_POINT ( 'NONE',  ( 9.609486011791450011, 8.908497650347621644, 0.000000000000000000 ) ) ;
#29274=CARTESIAN_POINT ( 'NONE',  ( -5.155570458487308549, 6.081290275064629824, -4.999999999999999112 ) ) ;
#29298=CARTESIAN_POINT ( 'NONE',  ( 8.830611806797369567, 133.7952729321875438, 6.141763964344532733E-13 ) ) ;
#29329=ORIENTED_EDGE ( 'NONE', *, *, #40738, .F. ) ;
#29381=CARTESIAN_POINT ( 'NONE',  ( 4.086350204929704688, 13.71221235928050497, 5.000000000000000888 ) ) ;
#29523=CARTESIAN_POINT ( 'NONE',  ( -9.999142969110272006, 7.501227345713487260, 5.000000000000000888 ) ) ;
#29587=DIRECTION ( 'NONE',  ( 0.000000000000000000, 0.000000000000000000, 1.000000000000000000 ) ) ;
#29670=DIRECTION ( 'NONE',  ( -1.000000000000000000, 0.000000000000000000, 0.000000000000000000 ) ) ;
#29776=DIRECTION ( 'NONE',  ( -0.000000000000000000, -0.000000000000000000, -1.000000000000000000 ) ) ;
#29793=CARTESIAN_POINT ( 'NONE',  ( -8.473474469330019687, 27.00279687854979827, -5.000000000000000000 ) ) ;
#29819=CARTESIAN_POINT ( 'NONE',  ( -3.058374439072180095, 45.00124159115523526, -4.999999999999998224 ) ) ;
#29820=CARTESIAN_POINT ( 'NONE',  ( 4.086459164113057874, 138.2893333910580509, -5.000000000000000000 ) ) ;
#29870=SURFACE_STYLE_FILL_AREA ( #13637 ) ;
#29879=CARTESIAN_POINT ( 'NONE',  ( -9.609486011791419813, 143.0915023496522736, 0.000000000000000000 ) ) ;
#29946=FACE_OUTER_BOUND ( 'NONE', #105335, .T. ) ;
#29985=FACE_OUTER_BOUND ( 'NONE', #6042, .T. ) ;
#30034=CARTESIAN_POINT ( 'NONE',  ( -3.833148349061555216, 18.02117837737563377, 4.999999999999999112 ) ) ;
#30140=CARTESIAN_POINT ( 'NONE',  ( 9.609486011791425142, 143.0915023496523304, 0.000000000000000000 ) ) ;
#30144=CARTESIAN_POINT ( 'NONE',  ( -4.075111592545596295, 138.1305188241016424, 4.999999999999999112 ) ) ;
#30204=ORIENTED_EDGE ( 'NONE', *, *, #6526, .T. ) ;
#30228=( NAMED_UNIT ( * ) SI_UNIT ( $, .STERADIAN. ) SOLID_ANGLE_UNIT ( ) );
#30234=CARTESIAN_POINT ( 'NONE',  ( -8.671807383147852377, 21.54545697599958842, -0.000000000000000000 ) ) ;
#30272=CARTESIAN_POINT ( 'NONE',  ( 14.54015256618498242, 142.2617268803927288, 0.000000000000000000 ) ) ;
#30275=STYLED_ITEM ( 'NONE', ( #17633 ), #11922 ) ;
#30284=CARTESIAN_POINT ( 'NONE',  ( 9.413227697955839801, 10.29402594059818021, 0.000000000000000000 ) ) ;
#30309=CARTESIAN_POINT ( 'NONE',  ( -9.460558175396068137, 9.928212646412896802, -5.000000000000000888 ) ) ;
#30328=VERTEX_POINT ( 'NONE', #85279 ) ;
#30337=CARTESIAN_POINT ( 'NONE',  ( 8.361452242989621197, 121.1754334411836567, -4.999999999998772537 ) ) ;
#30363=COLOUR_RGB ( '', 0.40784314, 0.44705882, 0.49803922) ;
#30402=CARTESIAN_POINT ( 'NONE',  ( 3.443342638033501490, 27.85812572534835496, 5.000000000000000000 ) ) ;
#30428=EDGE_CURVE ( 'NONE', #74794, #97405, #23842, .T. ) ;
#30565=CARTESIAN_POINT ( 'NONE',  ( -8.757836645960713540, 19.71581191398818333, 4.999999999999364952 ) ) ;
#30580=CYLINDRICAL_SURFACE ( 'NONE', #88482, 5.000000000000002665 ) ;
#30598=ORIENTED_EDGE ( 'NONE', *, *, #76488, .T. ) ;
#30704=EDGE_CURVE ( 'NONE', #53832, #1254, #58222, .T. ) ;
#30714=DIRECTION ( 'NONE',  ( 0.000000000000000000, 0.000000000000000000, -1.000000000000000000 ) ) ;
#30783=UNCERTAINTY_MEASURE_WITH_UNIT (LENGTH_MEASURE( 1.000000000000000082E-05 ), #47651, 'distance_accuracy_value', 'NONE');
#30826=CARTESIAN_POINT ( 'NONE',  ( 9.609486011791426918, 143.0915023496523020, 0.000000000000000000 ) ) ;
#30851=DIRECTION ( 'NONE',  ( -1.000000000000000000, 0.000000000000000000, 0.000000000000000000 ) ) ;
#30852=CARTESIAN_POINT ( 'NONE',  ( -4.248647703895898964, 140.2890219024546354, -5.000000000000000000 ) ) ;
#30882=CARTESIAN_POINT ( 'NONE',  ( 9.300689189976395710, 11.36225021102802124, -5.000000000000920153 ) ) ;
#30892=ORIENTED_EDGE ( 'NONE', *, *, #22212, .F. ) ;
#30932=TOROIDAL_SURFACE ( 'NONE', #20638, 10.00000000000000000, 5.000000000000000000 ) ;
#30945=CARTESIAN_POINT ( 'NONE',  ( 3.225593670035021177, 36.35169002663055693, 5.000000000000000888 ) ) ;
#31108=CARTESIAN_POINT ( 'NONE',  ( -4.659683500038751980, 8.173702696792386035, 5.000000000000000000 ) ) ;
#31161=CARTESIAN_POINT ( 'NONE',  ( -9.896734177125578569, 7.425145793380092840, -1.133793817387026337 ) ) ;
#31214=EDGE_LOOP ( 'NONE', ( #51126, #81635, #854, #10865 ) ) ;
#31219=CARTESIAN_POINT ( 'NONE',  ( -4.262243690392171658, 11.54664116576832988, 4.999999999999999112 ) ) ;
#31240=CIRCLE ( 'NONE', #45013, 5.000000000000000000 ) ;
#31256=ADVANCED_FACE ( 'NONE', ( #21989 ), #66578, .T. ) ;
#31384=CARTESIAN_POINT ( 'NONE',  ( -8.340816975826685464, 120.4114851256039600, 2.540892575254900838E-12 ) ) ;
#31413=CARTESIAN_POINT ( 'NONE',  ( 9.240146679118391049, 12.02903014930353010, 0.000000000000000000 ) ) ;
#31448=EDGE_LOOP ( 'NONE', ( #65103, #56021 ) ) ;
#31472=CARTESIAN_POINT ( 'NONE',  ( 9.075061003897785028, 14.05394893824808555, 4.999999999999385381 ) ) ;
#31480=VERTEX_POINT ( 'NONE', #29189 ) ;
#31496=CARTESIAN_POINT ( 'NONE',  ( 2.849088492170980924, 81.66462479025911136, 5.000000000000000000 ) ) ;
#31584=CARTESIAN_POINT ( 'NONE',  ( 0.000000000000000000, 0.000000000000000000, -5.000000000000000000 ) ) ;
#31622=CARTESIAN_POINT ( 'NONE',  ( -10.01627249115706775, 7.476760474189255490, 5.000000000000000888 ) ) ;
#31733=FILL_AREA_STYLE ('',( #74283 ) ) ;
#31748=FILL_AREA_STYLE ('',( #91571 ) ) ;
#31801=CARTESIAN_POINT ( 'NONE',  ( 7.500000000000000888, 1.224646799147353256E-15, 5.000000000000000000 ) ) ;
#31893=AXIS2_PLACEMENT_3D ( 'NONE', #66291, #66832, #67890 ) ;
#31898=CARTESIAN_POINT ( 'NONE',  ( -4.468886067276133467, 142.4736706807960616, -5.000000000000000888 ) ) ;
#31928=CARTESIAN_POINT ( 'NONE',  ( 2.955800887866951943, 53.34171681442641955, -5.000000000000000000 ) ) ;
#31963=MECHANICAL_DESIGN_GEOMETRIC_PRESENTATION_REPRESENTATION('',(#97371),#14673);
#31989=( NAMED_UNIT ( * ) SI_UNIT ( $, .STERADIAN. ) SOLID_ANGLE_UNIT ( ) );
#32194=FILL_AREA_STYLE ('',( #39748 ) ) ;
#32203=PRESENTATION_STYLE_ASSIGNMENT (( #88826 ) ) ;
#32406=ORIENTED_EDGE ( 'NONE', *, *, #41556, .T. ) ;
#32412=EDGE_LOOP ( 'NONE', ( #74155, #26952, #45541, #10018 ) ) ;
#32436=CARTESIAN_POINT ( 'NONE',  ( -8.972157809039631005, 136.3338258388681652, -2.602085213997499507E-15 ) ) ;
#32445=ADVANCED_FACE ( 'NONE', ( #86878 ), #30932, .T. ) ;
#32468=CARTESIAN_POINT ( 'NONE',  ( 8.763463954874010753, 19.59837311309268060, -5.000000000000613731 ) ) ;
#32504=COLOUR_RGB ( '', 0.72549020, 0.75294118, 0.79215686) ;
#32530=CARTESIAN_POINT ( 'NONE',  ( 8.441095186762201052, 28.00979909688160063, 5.000000000003685052 ) ) ;
#32612=EDGE_LOOP ( 'NONE', ( #86539, #85793, #105193, #92507 ) ) ;
#32691=CARTESIAN_POINT ( 'NONE',  ( -5.939670878927854503, 4.581516962870602505, 5.000000000000000888 ) ) ;
#32696=DIRECTION ( 'NONE',  ( 0.000000000000000000, 0.000000000000000000, -1.000000000000000000 ) ) ;
#32703=CARTESIAN_POINT ( 'NONE',  ( -6.486091964843609503, 4.943792391109567141, 4.959578321183684579 ) ) ;
#32724=AXIS2_PLACEMENT_3D ( 'NONE', #7835, #40213, #48293 ) ;
#32744=( LENGTH_UNIT ( ) NAMED_UNIT ( * ) SI_UNIT ( .MILLI., .METRE. ) );
#32860=ORIENTED_EDGE ( 'NONE', *, *, #76700, .T. ) ;
#32907=SURFACE_SIDE_STYLE ('',( #29870 ) ) ;
#32969=ORIENTED_EDGE ( 'NONE', *, *, #10190, .T. ) ;
#33041=ORIENTED_EDGE ( 'NONE', *, *, #10109, .F. ) ;
#33060=CARTESIAN_POINT ( 'NONE',  ( 4.474875413805487590, 142.5213423678850120, 5.000000000000000888 ) ) ;
#33062=DIRECTION ( 'NONE',  ( 0.8308658609248572580, 0.5564727496918389082, 0.000000000000000000 ) ) ;
#33101=SURFACE_STYLE_USAGE ( .BOTH. , #134 ) ;
#33212=CARTESIAN_POINT ( 'NONE',  ( -10.00002837220453600, 7.499959371249889983, 5.000000000000000888 ) ) ;
#33328=SURFACE_SIDE_STYLE ('',( #82917 ) ) ;
#33395=DIRECTION ( 'NONE',  ( -1.000000000000000000, 0.000000000000000000, 0.000000000000000000 ) ) ;
#33529=VERTEX_POINT ( 'NONE', #9786 ) ;
#33621=CARTESIAN_POINT ( 'NONE',  ( -10.04799450895598412, 7.431456737699888571, -5.000000000000000888 ) ) ;
#33649=CARTESIAN_POINT ( 'NONE',  ( 0.000000000000000000, 0.000000000000000000, 0.000000000000000000 ) ) ;
#33730=ORIENTED_EDGE ( 'NONE', *, *, #67896, .T. ) ;
#33747=CARTESIAN_POINT ( 'NONE',  ( -9.999586304443505824, 7.500591597926683285, 5.000000000000000888 ) ) ;
#33758=DIRECTION ( 'NONE',  ( -0.8308658609248562588, -0.5564727496918402405, 0.000000000000000000 ) ) ;
#33761=CARTESIAN_POINT ( 'NONE',  ( -9.172606077037439576, 6.899872791988882703, 3.046639664573870476 ) ) ;
#33838=TOROIDAL_SURFACE ( 'NONE', #13076, 7.500000000000006217, 5.000000000000000000 ) ;
#34037=FILL_AREA_STYLE_COLOUR ( '', #30363 ) ;
#34115=( NAMED_UNIT ( * ) PLANE_ANGLE_UNIT ( ) SI_UNIT ( $, .RADIAN. ) );
#34159=AXIS2_PLACEMENT_3D ( 'NONE', #6997, #47455, #80349 ) ;
#34164=CARTESIAN_POINT ( 'NONE',  ( -10.01459525654357030, 7.479155813459358093, -4.999999999999987566 ) ) ;
#34192=CARTESIAN_POINT ( 'NONE',  ( -5.126029744276100253, 6.171265713471635550, -4.999999999999998224 ) ) ;
#34314=ORIENTED_EDGE ( 'NONE', *, *, #37396, .T. ) ;
#34406=CARTESIAN_POINT ( 'NONE',  ( -7.500000000000000888, 0.000000000000000000, 0.000000000000000000 ) ) ;
#34414=UNCERTAINTY_MEASURE_WITH_UNIT (LENGTH_MEASURE( 1.000000000000000082E-05 ), #38276, 'distance_accuracy_value', 'NONE');
#34424=CARTESIAN_POINT ( 'NONE',  ( -8.241419208061959267, 35.69988999158593401, 5.000000000002541078 ) ) ;
#34457=LINE ( 'NONE', #34981, #71979 ) ;
#34473=ORIENTED_EDGE ( 'NONE', *, *, #64345, .F. ) ;
#34582=EDGE_CURVE ( 'NONE', #1352, #94076, #13850, .T. ) ;
#34678=CARTESIAN_POINT ( 'NONE',  ( -7.500000000000006217, 152.0000000000000000, 5.000000000000000000 ) ) ;
#34701=CARTESIAN_POINT ( 'NONE',  ( -9.995757844698658801, 7.506119843431433125, -4.999999999999999112 ) ) ;
#34717=FILL_AREA_STYLE ('',( #92909 ) ) ;
#34870=CARTESIAN_POINT ( 'NONE',  ( 3.996126808948458731, 15.12551640256268826, -4.999999999999999112 ) ) ;
#34947=CARTESIAN_POINT ( 'NONE',  ( -8.203754751779342769, 114.5734753959361711, -1.270355564599584843E-12 ) ) ;
#34950=CARTESIAN_POINT ( 'NONE',  ( 9.609486011791426918, 143.0915023496523020, 0.000000000000000000 ) ) ;
#34981=CARTESIAN_POINT ( 'NONE',  ( 5.000000000000000888, 6.123233995736767268E-16, 5.000000000000000000 ) ) ;
#35052=CARTESIAN_POINT ( 'NONE',  ( 3.168333439191699075, 112.8173450435234315, 5.000000000000000000 ) ) ;
#35225=CARTESIAN_POINT ( 'NONE',  ( -10.11479301378072648, 7.336058586181090746, -5.000000000000000888 ) ) ;
#35237=SURFACE_STYLE_FILL_AREA ( #34717 ) ;
#35413=EDGE_CURVE ( 'NONE', #83609, #1254, #73203, .T. ) ;
#35482=CARTESIAN_POINT ( 'NONE',  ( -7.883792884241596965, 61.98032949400206348, 0.000000000000000000 ) ) ;
#35562=CIRCLE ( 'NONE', #2799, 5.000000000000000000 ) ;
#35585=CARTESIAN_POINT ( 'NONE',  ( 3.443379947490608828, 124.1431617552111817, 4.999999999999999112 ) ) ;
#35588=CIRCLE ( 'NONE', #95844, 5.000000000000000888 ) ;
#35676=EDGE_CURVE ( 'NONE', #33529, #96258, #57806, .T. ) ;
#35682=ORIENTED_EDGE ( 'NONE', *, *, #131, .F. ) ;
#35706=EDGE_CURVE ( 'NONE', #80759, #44815, #38895, .T. ) ;
#35772=SURFACE_SIDE_STYLE ('',( #2816 ) ) ;
#35773=CARTESIAN_POINT ( 'NONE',  ( -9.999497344909480390, 7.500719060593830534, 0.000000000000000000 ) ) ;
#35859=FACE_OUTER_BOUND ( 'NONE', #97815, .T. ) ;
#35883=( LENGTH_UNIT ( ) NAMED_UNIT ( * ) SI_UNIT ( .MILLI., .METRE. ) );
#35893=AXIS2_PLACEMENT_3D ( 'NONE', #62143, #95542, #28724 ) ;
#36025=CARTESIAN_POINT ( 'NONE',  ( -8.745545711746213868, 132.0170111787129201, -6.344649108150348220E-13 ) ) ;
#36132=CARTESIAN_POINT ( 'NONE',  ( 3.591939471459422162, 128.3897234052070928, 4.999999999999999112 ) ) ;
#36181=ORIENTED_EDGE ( 'NONE', *, *, #69207, .T. ) ;
#36233=CARTESIAN_POINT ( 'NONE',  ( -9.047759419560607697, 14.48369194312116548, 1.733336949948506312E-30 ) ) ;
#36309=( LENGTH_UNIT ( ) NAMED_UNIT ( * ) SI_UNIT ( .MILLI., .METRE. ) );
#36310=CARTESIAN_POINT ( 'NONE',  ( -4.782240561419170533, 7.495540900963799658, -5.000000000000000888 ) ) ;
#36335=CARTESIAN_POINT ( 'NONE',  ( 8.588409832220163409, 128.2015064896677643, 0.000000000000000000 ) ) ;
#36439=EDGE_CURVE ( 'NONE', #52915, #12822, #72681, .T. ) ;
#36444=COLOUR_RGB ( '', 0.66274510, 0.83137255, 0.94901961) ;
#36530=CIRCLE ( 'NONE', #98515, 5.000000000000002665 ) ;
#36555=CARTESIAN_POINT ( 'NONE',  ( -7.883792884227283082, 61.98032949398166380, 5.000000000000000888 ) ) ;
#36583=ADVANCED_FACE ( 'NONE', ( #29946 ), #56160, .T. ) ;
#36625=ORIENTED_EDGE ( 'NONE', *, *, #105352, .T. ) ;
#36644=CARTESIAN_POINT ( 'NONE',  ( 0.000000000000000000, 152.0000000000000000, 0.000000000000000000 ) ) ;
#36658=CARTESIAN_POINT ( 'NONE',  ( 9.300689190519850769, 140.6377497888998391, 8.673617379410147005E-16 ) ) ;
#36785=VERTEX_POINT ( 'NONE', #85928 ) ;
#36829=CARTESIAN_POINT ( 'NONE',  ( -4.652400833064921137, 8.218796697697426268, -5.000000000000000888 ) ) ;
#36844=STYLED_ITEM ( 'NONE', ( #38415 ), #55083 ) ;
#36857=CARTESIAN_POINT ( 'NONE',  ( 7.955546711085375478, 98.60610140868929818, -5.000000000000000888 ) ) ;
#36931=AXIS2_PLACEMENT_3D ( 'NONE', #47281, #40260, #72625 ) ;
#36938=CARTESIAN_POINT ( 'NONE',  ( 3.363235851038136826, 30.69031363909868304, 5.000000000000000000 ) ) ;
#37061=DIRECTION ( 'NONE',  ( -0.000000000000000000, -0.000000000000000000, 1.000000000000000000 ) ) ;
#37081=CARTESIAN_POINT ( 'NONE',  ( -8.571529135618341400, 24.05510615524122642, 5.000000000001270095 ) ) ;
#37148=COLOUR_RGB ( '', 0.40784314, 0.44705882, 0.49803922) ;
#37186=CARTESIAN_POINT ( 'NONE',  ( -3.151705372620861478, 111.9488642000127356, 4.999999999999999112 ) ) ;
#37214=SURFACE_SIDE_STYLE ('',( #45811 ) ) ;
#37229=CARTESIAN_POINT ( 'NONE',  ( 0.000000000000000000, 152.0000000000000000, 0.000000000000000000 ) ) ;
#37332=CARTESIAN_POINT ( 'NONE',  ( 7.869023571503454662, 64.80998104766133849, 1.348150961071065097E-30 ) ) ;
#37342=VERTEX_POINT ( 'NONE', #31801 ) ;
#37344=B_SPLINE_CURVE_WITH_KNOTS ( 'NONE', 3,
 ( #28313, #104280, #77365, #77898, #103235, #29381, #94078, #20243, #95152, #86014, #36938, #87063, #61737, #87587, #13674, #46582, #81573, #31496, #41153, #105870, #40087, #63847, #15805, #7173, #72964, #8240, #96740, #105355, #47628, #15276, #57840, #74035, #57311, #7700 ),
 .UNSPECIFIED., .F., .F.,
 ( 4, 2, 2, 2, 2, 2, 2, 2, 2, 2, 2, 2, 2, 2, 2, 2, 4 ),
 ( 0.000000000000000000, 0.002123632632474336222, 0.004247265264948672445, 0.008494530529897344889, 0.01698906105979468978, 0.02548359158969203467, 0.03397812211958937956, 0.05096718317938406934, 0.06795624423917875911, 0.08494530529897345583, 0.1019343663587681387, 0.1104288968886654870, 0.1189234274185628215, 0.1274179579484601144, 0.1316652232134088163, 0.1337888558458831534, 0.1359124884783575182 ),
 .UNSPECIFIED. ) ;
#37358=CARTESIAN_POINT ( 'NONE',  ( -9.248416039967223057, 11.93391985751763151, -5.000000000000318856 ) ) ;
#37367=FILL_AREA_STYLE_COLOUR ( '', #81581 ) ;
#37389=CARTESIAN_POINT ( 'NONE',  ( -3.983822851467989423, 136.6779518951960881, -5.000000000000000888 ) ) ;
#37390=CARTESIAN_POINT ( 'NONE',  ( 4.474494503601499140, 142.5181942220502833, -4.999999999999999112 ) ) ;
#37396=EDGE_CURVE ( 'NONE', #12734, #65330, #56328, .T. ) ;
#37540=DIRECTION ( 'NONE',  ( 0.1659550938519105956, -0.9861333108787085910, -0.000000000000000000 ) ) ;
#37618=CARTESIAN_POINT ( 'NONE',  ( -5.452425833994689164, 5.376849860293315686, 5.000000000000000000 ) ) ;
#37652=CIRCLE ( 'NONE', #82412, 5.000000000000000000 ) ;
#37722=CARTESIAN_POINT ( 'NONE',  ( 9.518114778805811582, 142.5485589762550092, 5.000000000000000888 ) ) ;
#37726=DIRECTION ( 'NONE',  ( -1.224646799147353207E-16, 1.000000000000000000, 0.000000000000000000 ) ) ;
#37790=SURFACE_STYLE_USAGE ( .BOTH. , #53411 ) ;
#37816=SURFACE_SIDE_STYLE ('',( #71193 ) ) ;
#37820=FILL_AREA_STYLE ('',( #61548 ) ) ;
#37822=CARTESIAN_POINT ( 'NONE',  ( -9.411401105578752535, 141.6908105720070239, -0.000000000000000000 ) ) ;
#37890=CARTESIAN_POINT ( 'NONE',  ( -8.985503746895339816, 15.44863866162878452, 0.000000000000000000 ) ) ;
#37906=EDGE_CURVE ( 'NONE', #39330, #83609, #89156, .T. ) ;
#37919=CARTESIAN_POINT ( 'NONE',  ( 8.642223818570965221, 129.6034357518176989, 0.000000000000000000 ) ) ;
#38052=( LENGTH_UNIT ( ) NAMED_UNIT ( * ) SI_UNIT ( .MILLI., .METRE. ) );
#38143=CARTESIAN_POINT ( 'NONE',  ( -3.477260921866647703, 26.80326629624875423, 5.000000000000000000 ) ) ;
#38276=( LENGTH_UNIT ( ) NAMED_UNIT ( * ) SI_UNIT ( .MILLI., .METRE. ) );
#38284=SURFACE_STYLE_USAGE ( .BOTH. , #6936 ) ;
#38335=DIRECTION ( 'NONE',  ( -1.000000000000000000, 0.000000000000000000, 0.000000000000000000 ) ) ;
#38337=CIRCLE ( 'NONE', #98580, 12.50000000000000533 ) ;
#38338=CARTESIAN_POINT ( 'NONE',  ( -9.609486011791419813, 143.0915023496522736, 0.000000000000000000 ) ) ;
#38380=CARTESIAN_POINT ( 'NONE',  ( 8.731365433225425576, 20.06141188278254006, -2.602085213965209853E-15 ) ) ;
#38404=CARTESIAN_POINT ( 'NONE',  ( -9.737904753430131066, 8.235624462465031215, -5.000000000000000888 ) ) ;
#38415=PRESENTATION_STYLE_ASSIGNMENT (( #86442 ) ) ;
#38435=CARTESIAN_POINT ( 'NONE',  ( 7.869427812662811661, 87.30462500886650901, 0.000000000000000000 ) ) ;
#38626=EDGE_LOOP ( 'NONE', ( #8888, #56651, #30598, #2101 ) ) ;
#38651=CARTESIAN_POINT ( 'NONE',  ( -9.946294134353090399, 7.586021175265231342, 5.000000000000000888 ) ) ;
#38692=CARTESIAN_POINT ( 'NONE',  ( 3.021265037602215209, 104.3213281748178360, -4.999999999999999112 ) ) ;
#38698=ORIENTED_EDGE ( 'NONE', *, *, #46079, .T. ) ;
#38703=EDGE_CURVE ( 'NONE', #105180, #18064, #70300, .T. ) ;
#38704=CARTESIAN_POINT ( 'NONE',  ( -9.742555539022085043, 7.313362239096417916, -1.762132461011677309 ) ) ;
#38786=CARTESIAN_POINT ( 'NONE',  ( 0.000000000000000000, 0.000000000000000000, 0.000000000000000000 ) ) ;
#38800=CARTESIAN_POINT ( 'NONE',  ( 0.000000000000000000, 152.0000000000000000, 0.000000000000000000 ) ) ;
#38857=ORIENTED_EDGE ( 'NONE', *, *, #76488, .F. ) ;
#38895=CIRCLE ( 'NONE', #45737, 5.000000000000000888 ) ;
#38899=CARTESIAN_POINT ( 'NONE',  ( 9.493245307752808060, 9.599219626221964674, -0.000000000000000000 ) ) ;
#38922=CARTESIAN_POINT ( 'NONE',  ( -2.856083322019343118, 67.83493845259130239, -5.000000000000000000 ) ) ;
#38943=DIRECTION ( 'NONE',  ( 0.5564727496918440153, 0.8308658609248538163, 0.000000000000000000 ) ) ;
#38949=CARTESIAN_POINT ( 'NONE',  ( 8.642300018659421212, 22.39467290678169320, -4.999999999999385381 ) ) ;
#38976=( GEOMETRIC_REPRESENTATION_CONTEXT ( 3 ) GLOBAL_UNCERTAINTY_ASSIGNED_CONTEXT ( ( #30783 ) ) GLOBAL_UNIT_ASSIGNED_CONTEXT ( ( #47651, #2817, #93445 ) ) REPRESENTATION_CONTEXT ( 'NONE', 'WORKASPACE' ) );
#39012=CARTESIAN_POINT ( 'NONE',  ( 9.439237903447189382, 10.07757316350726207, 9.227579807199164141E-13 ) ) ;
#39129=VECTOR ( 'NONE', #92099, 1000.000000000000000 ) ;
#39179=CARTESIAN_POINT ( 'NONE',  ( -9.971054623845207132, 7.543597283302578838, 4.999999999999846345 ) ) ;
#39257=EDGE_LOOP ( 'NONE', ( #84359, #90275, #3842, #72501 ) ) ;
#39292=CARTESIAN_POINT ( 'NONE',  ( -3.949145016516434126, 15.90303839293037669, 5.000000000000000888 ) ) ;
#39330=VERTEX_POINT ( 'NONE', #34678 ) ;
#39441=( NAMED_UNIT ( * ) SI_UNIT ( $, .STERADIAN. ) SOLID_ANGLE_UNIT ( ) );
#39458=CARTESIAN_POINT ( 'NONE',  ( -9.061861678845534840, 137.7616487646043311, 0.000000000000000000 ) ) ;
#39487=CARTESIAN_POINT ( 'NONE',  ( 8.830661707197100085, 18.20374273969819257, -9.201869806248672558E-30 ) ) ;
#39549=CARTESIAN_POINT ( 'NONE',  ( 9.239881047873428344, 12.03209342863740972, 3.069484470019327247E-13 ) ) ;
#39621=FILL_AREA_STYLE_COLOUR ( '', #28685 ) ;
#39719=( GEOMETRIC_REPRESENTATION_CONTEXT ( 3 ) GLOBAL_UNCERTAINTY_ASSIGNED_CONTEXT ( ( #79012 ) ) GLOBAL_UNIT_ASSIGNED_CONTEXT ( ( #24814, #70307, #62239 ) ) REPRESENTATION_CONTEXT ( 'NONE', 'WORKASPACE' ) );
#39744=SURFACE_STYLE_FILL_AREA ( #73135 ) ;
#39748=FILL_AREA_STYLE_COLOUR ( '', #15260 ) ;
#39758=FILL_AREA_STYLE_COLOUR ( '', #37148 ) ;
#39770=( GEOMETRIC_REPRESENTATION_CONTEXT ( 3 ) GLOBAL_UNCERTAINTY_ASSIGNED_CONTEXT ( ( #1954 ) ) GLOBAL_UNIT_ASSIGNED_CONTEXT ( ( #85242, #52868, #86328 ) ) REPRESENTATION_CONTEXT ( 'NONE', 'WORKASPACE' ) );
#39822=UNCERTAINTY_MEASURE_WITH_UNIT (LENGTH_MEASURE( 1.000000000000000082E-05 ), #36309, 'distance_accuracy_value', 'NONE');
#39853=ADVANCED_FACE ( 'NONE', ( #14470 ), #89389, .T. ) ;
#39976=CARTESIAN_POINT ( 'NONE',  ( -3.148155568693087769, 111.7595494157684612, -5.000000000000000000 ) ) ;
#40005=CARTESIAN_POINT ( 'NONE',  ( 8.986804597294771213, 15.43199845812625703, -5.000000000000000888 ) ) ;
#40061=CARTESIAN_POINT ( 'NONE',  ( 8.588409832221012508, 23.79849351030796711, -1.228354175402838067E-12 ) ) ;
#40087=CARTESIAN_POINT ( 'NONE',  ( 3.021254343616690097, 104.3205651224084249, 4.999999999999999112 ) ) ;
#40156=( GEOMETRIC_REPRESENTATION_CONTEXT ( 3 ) GLOBAL_UNCERTAINTY_ASSIGNED_CONTEXT ( ( #11397 ) ) GLOBAL_UNIT_ASSIGNED_CONTEXT ( ( #40329, #72693, #14980 ) ) REPRESENTATION_CONTEXT ( 'NONE', 'WORKASPACE' ) );
#40213=DIRECTION ( 'NONE',  ( -0.000000000000000000, -0.000000000000000000, -1.000000000000000000 ) ) ;
#40231=CARTESIAN_POINT ( 'NONE',  ( -9.999999999999994671, 7.499999999999983125, 0.3301729510373770382 ) ) ;
#40260=DIRECTION ( 'NONE',  ( 0.000000000000000000, 0.000000000000000000, -1.000000000000000000 ) ) ;
#40329=( LENGTH_UNIT ( ) NAMED_UNIT ( * ) SI_UNIT ( .MILLI., .METRE. ) );
#40493=AXIS2_PLACEMENT_3D ( 'NONE', #58435, #7739, #58975 ) ;
#40499=CARTESIAN_POINT ( 'NONE',  ( -8.147310229341139021, 111.6670789908538381, -1.269956413672949300E-12 ) ) ;
#40528=CARTESIAN_POINT ( 'NONE',  ( 9.075140001326078121, 14.05259049549145978, 0.000000000000000000 ) ) ;
#40542=LINE ( 'NONE', #15735, #7912 ) ;
#40588=CARTESIAN_POINT ( 'NONE',  ( 3.836943873307946173, 17.95160350248317371, 4.999999999999999112 ) ) ;
#40738=EDGE_CURVE ( 'NONE', #61174, #53832, #68610, .T. ) ;
#40744=CARTESIAN_POINT ( 'NONE',  ( -5.906143312800266720, 4.629399289606634937, 4.999999999999999112 ) ) ;
#40756=CARTESIAN_POINT ( 'NONE',  ( -7.008653203440415425, 5.325399036039260459, 4.838637849014732595 ) ) ;
#40859=CARTESIAN_POINT ( 'NONE',  ( -5.252396211958147099, 5.824410605298178112, 4.999999999999999112 ) ) ;
#40878=SURFACE_STYLE_FILL_AREA ( #31748 ) ;
#41032=CARTESIAN_POINT ( 'NONE',  ( -8.002730990595935623, 102.9130261956175758, 2.539912827345902235E-12 ) ) ;
#41067=AXIS2_PLACEMENT_3D ( 'NONE', #31584, #97338, #66043 ) ;
#41125=CARTESIAN_POINT ( 'NONE',  ( 9.075140000863360257, 137.9474095045275988, 4.999999999999385381 ) ) ;
#41153=CARTESIAN_POINT ( 'NONE',  ( 2.869469304594359560, 87.32891902835181952, 5.000000000000000000 ) ) ;
#41276=COLOUR_RGB ( '', 0.72549020, 0.75294118, 0.79215686) ;
#41277=CARTESIAN_POINT ( 'NONE',  ( -10.52078253383812267, 6.756245462352919340, 0.000000000000000000 ) ) ;
#41370=ADVANCED_FACE ( 'NONE', ( #98876 ), #104850, .T. ) ;
#41406=CARTESIAN_POINT ( 'NONE',  ( -9.609486011791419813, 143.0915023496522736, 2.602085213965210642E-15 ) ) ;
#41428=EDGE_CURVE ( 'NONE', #88114, #39330, #53200, .T. ) ;
#41556=EDGE_CURVE ( 'NONE', #70327, #1352, #50095, .T. ) ;
#41805=CARTESIAN_POINT ( 'NONE',  ( -10.04820350651657890, 7.431158258250313509, 0.000000000000000000 ) ) ;
#41823=CARTESIAN_POINT ( 'NONE',  ( -8.425387792203615334, 6.357088691644186440, 3.972068509340369147 ) ) ;
#42101=DIRECTION ( 'NONE',  ( 0.000000000000000000, 0.000000000000000000, 1.000000000000000000 ) ) ;
#42182=AXIS2_PLACEMENT_3D ( 'NONE', #58614, #76367, #100120 ) ;
#42232=ORIENTED_EDGE ( 'NONE', *, *, #63842, .T. ) ;
#42270=UNCERTAINTY_MEASURE_WITH_UNIT (LENGTH_MEASURE( 1.000000000000000082E-05 ), #5767, 'distance_accuracy_value', 'NONE');
#42377=( NAMED_UNIT ( * ) SI_UNIT ( $, .STERADIAN. ) SOLID_ANGLE_UNIT ( ) );
#42386=CARTESIAN_POINT ( 'NONE',  ( 2.869469963220364406, 87.32917479646899039, -4.999999999999998224 ) ) ;
#42686=UNCERTAINTY_MEASURE_WITH_UNIT (LENGTH_MEASURE( 1.000000000000000082E-05 ), #58899, 'distance_accuracy_value', 'NONE');
#42921=CARTESIAN_POINT ( 'NONE',  ( 0.000000000000000000, 0.000000000000000000, 0.000000000000000000 ) ) ;
#42933=ORIENTED_EDGE ( 'NONE', *, *, #28052, .F. ) ;
#43014=CARTESIAN_POINT ( 'NONE',  ( -7.939583658500668939, 97.05573068118653168, 5.000000000002541078 ) ) ;
#43055=CARTESIAN_POINT ( 'NONE',  ( -7.500000000000006217, 152.0000000000000000, -5.000000000000000000 ) ) ;
#43114=CARTESIAN_POINT ( 'NONE',  ( 3.646260779474320035, 129.8050105372081475, 5.000000000000000888 ) ) ;
#43172=CARTESIAN_POINT ( 'NONE',  ( 5.000000000000002665, 152.0000000000000000, 5.000000000000000000 ) ) ;
#43230=MECHANICAL_DESIGN_GEOMETRIC_PRESENTATION_REPRESENTATION('',(#19177),#39770);
#43288=CARTESIAN_POINT ( 'NONE',  ( -10.54230344465946345, 6.725510416460146246, 0.000000000000000000 ) ) ;
#43508=CARTESIAN_POINT ( 'NONE',  ( 0.000000000000000000, 0.000000000000000000, 5.000000000000000000 ) ) ;
#43544=CARTESIAN_POINT ( 'NONE',  ( -7.860264365974899192, 85.36576122642846087, 4.999999999997459810 ) ) ;
#43610=CARTESIAN_POINT ( 'NONE',  ( 0.000000000000000000, 152.0000000000000000, 0.000000000000000000 ) ) ;
#43640=CARTESIAN_POINT ( 'NONE',  ( 7.955551520407984079, 98.60650887776563422, 0.000000000000000000 ) ) ;
#43674=ADVANCED_FACE ( 'NONE', ( #85342 ), #49578, .T. ) ;
#43731=( GEOMETRIC_REPRESENTATION_CONTEXT ( 3 ) GLOBAL_UNCERTAINTY_ASSIGNED_CONTEXT ( ( #20135 ) ) GLOBAL_UNIT_ASSIGNED_CONTEXT ( ( #62164, #55084, #21189 ) ) REPRESENTATION_CONTEXT ( 'NONE', 'WORKASPACE' ) );
#43806=APPLICATION_CONTEXT ( 'automotive_design' ) ;
#43808=B_SPLINE_CURVE_WITH_KNOTS ( 'NONE', 3,
 ( #62501, #88369, #21017, #71108, #102953, #30144, #53858, #79729, #86787, #95925, #12332, #45258, #37186, #95389, #22598, #21529, #54909, #14444, #87836, #71626, #70048, #45776, #29117, #47357, #80245, #6351, #54361, #39292, #72171, #64103, #31219, #90480, #57030, #65672, #64619, #89427, #74807, #66738, #40859, #48933, #57554, #98556, #48410, #106648 ),
 .UNSPECIFIED., .F., .F.,
 ( 4, 2, 2, 2, 2, 2, 2, 2, 2, 2, 2, 2, 2, 2, 2, 2, 2, 2, 2, 2, 2, 4 ),
 ( 0.000000000000000000, 0.002182755796778808495, 0.004365511593557616990, 0.008731023187115233980, 0.01746204637423055470, 0.02619306956134582684, 0.03492409274846109551, 0.05238613912269164674, 0.06984818549692217715, 0.08731023187115276307, 0.1047722782453833629, 0.1135033014324986628, 0.1222343246196139349, 0.1265998362131715849, 0.1309653478067292209, 0.1331481036035080667, 0.1353308594002868848, 0.1364222372986763077, 0.1375136151970657306, 0.1386049930954551257, 0.1391506820446498371, 0.1396963709938445486 ),
 .UNSPECIFIED. ) ;
#43814=CARTESIAN_POINT ( 'NONE',  ( -10.54230344465946168, 6.725510416460146246, -5.000000000000000888 ) ) ;
#43828=PRESENTATION_STYLE_ASSIGNMENT (( #61094 ) ) ;
#43972=CARTESIAN_POINT ( 'NONE',  ( 0.000000000000000000, 0.000000000000000000, 0.000000000000000000 ) ) ;
#44078=CARTESIAN_POINT ( 'NONE',  ( -4.072633637071363388, 138.0955724161418061, 4.999999999999997335 ) ) ;
#44182=CARTESIAN_POINT ( 'NONE',  ( 2.849086893377218654, 70.33581626579710644, 5.000000000000000000 ) ) ;
#44356=CARTESIAN_POINT ( 'NONE',  ( -5.902135779713443497, 4.635123429159628827, -5.000000000000000000 ) ) ;
#44385=CARTESIAN_POINT ( 'NONE',  ( 4.561000490391409201, 143.2211774994303255, -5.000000000000000888 ) ) ;
#44412=DIRECTION ( 'NONE',  ( -1.000000000000000000, 0.000000000000000000, 0.000000000000000000 ) ) ;
#44422=ORIENTED_EDGE ( 'NONE', *, *, #23994, .T. ) ;
#44531=VERTEX_POINT ( 'NONE', #86448 ) ;
#44577=ADVANCED_FACE ( 'NONE', ( #14096 ), #4973, .F. ) ;
#44611=AXIS2_PLACEMENT_3D ( 'NONE', #98185, #56654, #90099 ) ;
#44620=CARTESIAN_POINT ( 'NONE',  ( -8.340586800768058140, 120.4027948985844176, 1.270355564599584843E-12 ) ) ;
#44722=CARTESIAN_POINT ( 'NONE',  ( 9.240146679119453310, 139.9709698507093947, -3.072172964960699772E-13 ) ) ;
#44815=VERTEX_POINT ( 'NONE', #1625 ) ;
#44830=CARTESIAN_POINT ( 'NONE',  ( -9.716937824887432740, 8.335377965868620009, -0.000000000000000000 ) ) ;
#44854=AXIS2_PLACEMENT_3D ( 'NONE', #96307, #22436, #88205 ) ;
#44901=CARTESIAN_POINT ( 'NONE',  ( -3.067150697641109591, 44.40839135605776988, -5.000000000000000000 ) ) ;
#44929=CARTESIAN_POINT ( 'NONE',  ( -3.006283056400744780, 103.2180882720525545, -4.999999999999999112 ) ) ;
#44930=CARTESIAN_POINT ( 'NONE',  ( 8.830611806671452513, 133.7952729321947061, -4.999999999999385381 ) ) ;
#44957=CARTESIAN_POINT ( 'NONE',  ( 0.000000000000000000, 152.0000000000000000, 5.000000000000000000 ) ) ;
#45013=AXIS2_PLACEMENT_3D ( 'NONE', #66785, #99671, #73249 ) ;
#45060=CARTESIAN_POINT ( 'NONE',  ( -5.956988534971662475, 4.556784786910193397, -5.000000000000000000 ) ) ;
#45129=EDGE_LOOP ( 'NONE', ( #56751, #68425, #1829, #77871 ) ) ;
#45152=CARTESIAN_POINT ( 'NONE',  ( -8.067121135810884525, 44.45135178119092956, 4.999999999994918731 ) ) ;
#45258=CARTESIAN_POINT ( 'NONE',  ( -3.208644920884031304, 114.8591176307894415, 5.000000000000000000 ) ) ;
#45325=CARTESIAN_POINT ( 'NONE',  ( 0.000000000000000000, 152.0000000000000000, 0.000000000000000000 ) ) ;
#45350=PLANE ( 'NONE',  #51924 ) ;
#45399=CARTESIAN_POINT ( 'NONE',  ( 8.160631864331239882, 112.3644544865306898, -0.000000000000000000 ) ) ;
#45428=CARTESIAN_POINT ( 'NONE',  ( -9.686785446062245342, 8.472505610524187603, 0.000000000000000000 ) ) ;
#45455=CARTESIAN_POINT ( 'NONE',  ( 9.075061004355355010, 137.9460510617185491, 0.000000000000000000 ) ) ;
#45541=ORIENTED_EDGE ( 'NONE', *, *, #75261, .F. ) ;
#45675=CARTESIAN_POINT ( 'NONE',  ( -9.252395038874292155, 11.88928468661912596, 5.000000000000317080 ) ) ;
#45737=AXIS2_PLACEMENT_3D ( 'NONE', #70244, #38943, #88026 ) ;
#45776=CARTESIAN_POINT ( 'NONE',  ( -3.227781575335565645, 36.26785195737000578, 5.000000000000000888 ) ) ;
#45811=SURFACE_STYLE_FILL_AREA ( #46340 ) ;
#45921=CARTESIAN_POINT ( 'NONE',  ( 7.953361656945785008, 53.62094058914818362, 1.444447458290428860E-31 ) ) ;
#45948=CARTESIAN_POINT ( 'NONE',  ( -8.570032633590477289, 24.09669418279240816, -1.270257828436642457E-12 ) ) ;
#45979=CARTESIAN_POINT ( 'NONE',  ( -3.794165308086080213, 18.81398966773962300, -5.000000000000000000 ) ) ;
#45980=CARTESIAN_POINT ( 'NONE',  ( 8.642223818515795131, 129.6034357518201148, -4.999999999999999112 ) ) ;
#46079=EDGE_CURVE ( 'NONE', #10915, #36785, #48180, .T. ) ;
#46168=CARTESIAN_POINT ( 'NONE',  ( -14.54015256618497176, 142.2617268803927573, 5.000000000000000000 ) ) ;
#46204=CARTESIAN_POINT ( 'NONE',  ( -4.604390456819611011, 8.535337771752283587, 5.000000000000000000 ) ) ;
#46217=DIRECTION ( 'NONE',  ( -0.000000000000000000, -0.000000000000000000, -1.000000000000000000 ) ) ;
#46300=CARTESIAN_POINT ( 'NONE',  ( -5.000000000000000888, 0.000000000000000000, 5.000000000000000000 ) ) ;
#46316=CLOSED_SHELL ( 'NONE', ( #39853, #26428, #36583, #87638, #19117, #95259, #102828, #41370, #54694, #90576, #93079, #56902, #90864, #44577, #72138, #31256, #14716, #11922, #97466, #9496, #85004, #93400, #79708, #17821, #14500, #32445, #43674, #96183 ) ) ;
#46340=FILL_AREA_STYLE ('',( #87866 ) ) ;
#46404=( NAMED_UNIT ( * ) SI_UNIT ( $, .STERADIAN. ) SOLID_ANGLE_UNIT ( ) );
#46408=CARTESIAN_POINT ( 'NONE',  ( -7.847409547159631238, 80.92320383547315998, 4.333342374871287676E-31 ) ) ;
#46475=CARTESIAN_POINT ( 'NONE',  ( -9.076657995136841350, 14.02231722287513804, 6.347424771477776860E-13 ) ) ;
#46500=CARTESIAN_POINT ( 'NONE',  ( 8.167402502808952747, 112.7203465494860097, 0.000000000000000000 ) ) ;
#46549=ORIENTED_EDGE ( 'NONE', *, *, #100457, .F. ) ;
#46582=CARTESIAN_POINT ( 'NONE',  ( 2.869469963220363962, 64.67082520353208963, 5.000000000000000000 ) ) ;
#46657=TOROIDAL_SURFACE ( 'NONE', #48329, 10.00000000000000000, 5.000000000000000000 ) ;
#46689=AXIS2_PLACEMENT_3D ( 'NONE', #45325, #21600, #102493 ) ;
#46705=CARTESIAN_POINT ( 'NONE',  ( 4.678819457397886517, 143.9212778189118467, 0.000000000000000000 ) ) ;
#46721=CARTESIAN_POINT ( 'NONE',  ( -4.460880975709559770, 9.623342354847359559, 4.999999999999999112 ) ) ;
#46765=CARTESIAN_POINT ( 'NONE',  ( 3.363235851038141710, 121.3096863609017078, -5.000000000000000000 ) ) ;
#46840=ORIENTED_EDGE ( 'NONE', *, *, #64345, .T. ) ;
#46970=PRESENTATION_STYLE_ASSIGNMENT (( #96073 ) ) ;
#46989=CARTESIAN_POINT ( 'NONE',  ( -4.267972493540475476, 11.49087057789210853, -5.000000000000000888 ) ) ;
#47016=CARTESIAN_POINT ( 'NONE',  ( 3.646260779472994429, 22.19498946286545760, -5.000000000000000000 ) ) ;
#47077=CARTESIAN_POINT ( 'NONE',  ( 8.167402502815940935, 39.27965345049515378, 4.999999999998771649 ) ) ;
#47099=FILL_AREA_STYLE ('',( #82119 ) ) ;
#47137=CARTESIAN_POINT ( 'NONE',  ( 0.000000000000000000, 152.0000000000000000, -5.000000000000000000 ) ) ;
#47166=DIRECTION ( 'NONE',  ( -0.9861333108787084800, -0.1659550938519104846, 0.000000000000000000 ) ) ;
#47202=EDGE_LOOP ( 'NONE', ( #39, #46840, #91367, #32969 ) ) ;
#47240=CARTESIAN_POINT ( 'NONE',  ( -9.838569038458777172, 7.857203345964940411, 0.000000000000000000 ) ) ;
#47281=CARTESIAN_POINT ( 'NONE',  ( -14.54015256618497176, 142.2617268803927573, 0.000000000000000000 ) ) ;
#47290=AXIS2_PLACEMENT_3D ( 'NONE', #92336, #18481, #60012 ) ;
#47341=COLOUR_RGB ( '', 0.09019608, 0.27058824, 0.51372549) ;
#47357=CARTESIAN_POINT ( 'NONE',  ( -3.454256172262368363, 27.53752580628883706, 4.999999999999998224 ) ) ;
#47455=DIRECTION ( 'NONE',  ( 0.1659550938513499052, -0.9861333108788029600, 5.742823393231985512E-13 ) ) ;
#47500=SURFACE_STYLE_FILL_AREA ( #79345 ) ;
#47521=CARTESIAN_POINT ( 'NONE',  ( -7.856068184137752652, 67.85260481710604097, 0.000000000000000000 ) ) ;
#47547=CARTESIAN_POINT ( 'NONE',  ( 3.363293968486921859, 30.68813792664008844, -4.999999999999997335 ) ) ;
#47585=ORIENTED_EDGE ( 'NONE', *, *, #24440, .T. ) ;
#47606=SURFACE_STYLE_USAGE ( .BOTH. , #64864 ) ;
#47624=CIRCLE ( 'NONE', #76891, 5.000000000000000888 ) ;
#47628=CARTESIAN_POINT ( 'NONE',  ( 4.086341046824350620, 138.2878350440129509, 4.999999999999999112 ) ) ;
#47646=CIRCLE ( 'NONE', #20146, 7.500000000000006217 ) ;
#47651=( LENGTH_UNIT ( ) NAMED_UNIT ( * ) SI_UNIT ( .MILLI., .METRE. ) );
#47662=EDGE_CURVE ( 'NONE', #31480, #105180, #12308, .T. ) ;
#47794=MECHANICAL_DESIGN_GEOMETRIC_PRESENTATION_REPRESENTATION('',(#11621),#13389);
#47878=DIRECTION ( 'NONE',  ( 1.000000000000000000, 0.000000000000000000, 0.000000000000000000 ) ) ;
#47948=DIRECTION ( 'NONE',  ( 0.5564727496918402405, -0.8308658609248562588, -0.000000000000000000 ) ) ;
#48041=CARTESIAN_POINT ( 'NONE',  ( -8.203969886209304008, 114.5837526204806522, -2.539157851778924031E-12 ) ) ;
#48072=CARTESIAN_POINT ( 'NONE',  ( 8.763463954822906743, 19.59837311309046370, -1.228393653933357778E-12 ) ) ;
#48091=DIRECTION ( 'NONE',  ( 0.000000000000000000, 0.000000000000000000, -1.000000000000000000 ) ) ;
#48136=CARTESIAN_POINT ( 'NONE',  ( 8.830611806670223274, 18.20472706776127580, 4.999999999999999112 ) ) ;
#48180=CIRCLE ( 'NONE', #105100, 9.999999999999998224 ) ;
#48293=DIRECTION ( 'NONE',  ( -1.000000000000000000, 0.000000000000000000, 0.000000000000000000 ) ) ;
#48329=AXIS2_PLACEMENT_3D ( 'NONE', #54745, #95238, #5161 ) ;
#48339=SURFACE_STYLE_USAGE ( .BOTH. , #54839 ) ;
#48342=CARTESIAN_POINT ( 'NONE',  ( 4.258869285391234882, 140.4044011673899774, -5.000000000000000000 ) ) ;
#48410=CARTESIAN_POINT ( 'NONE',  ( -5.851594670652180419, 4.707302824160916721, 5.000000000000000000 ) ) ;
#48573=CARTESIAN_POINT ( 'NONE',  ( -9.230092720033631792, 139.8575112583843350, 0.000000000000000000 ) ) ;
#48604=CARTESIAN_POINT ( 'NONE',  ( 8.224467148766224867, 36.45870262746186086, 1.229177290248652582E-12 ) ) ;
#48662=CARTESIAN_POINT ( 'NONE',  ( 8.763392006798923717, 19.59990099439337996, 5.000000000000613731 ) ) ;
#48818=CARTESIAN_POINT ( 'NONE',  ( -10.52078253383812267, 6.756245462352918452, 5.000000000000000888 ) ) ;
#48834=CARTESIAN_POINT ( 'NONE',  ( -9.742515530865327733, 7.313333228401042163, 1.762264882286370682 ) ) ;
#48933=CARTESIAN_POINT ( 'NONE',  ( -5.482452937080444677, 5.333397824891131123, 5.000000000000000888 ) ) ;
#48949=CARTESIAN_POINT ( 'NONE',  ( -9.433863491267240775, 141.8798491995066797, 4.999999999999050537 ) ) ;
#49101=CARTESIAN_POINT ( 'NONE',  ( -3.422808420448540279, 123.4701245564265122, -4.999999999999999112 ) ) ;
#49166=COLOUR_RGB ( '', 0.66274510, 0.83137255, 0.94901961) ;
#49192=EDGE_CURVE ( 'NONE', #1352, #33529, #27555, .T. ) ;
#49197=CARTESIAN_POINT ( 'NONE',  ( 8.763463954820251089, 132.4016268868482200, 6.150641887046839534E-13 ) ) ;
#49251=AXIS2_PLACEMENT_3D ( 'NONE', #33649, #74076, #15851 ) ;
#49356=CARTESIAN_POINT ( 'NONE',  ( -6.220663814092025845, 4.180217462607255463, 5.000000000000000888 ) ) ;
#49409=CARTESIAN_POINT ( 'NONE',  ( 4.561148568382323631, 8.777942558635560388, -5.000000000000000000 ) ) ;
#49412=UNCERTAINTY_MEASURE_WITH_UNIT (LENGTH_MEASURE( 1.000000000000000082E-05 ), #95760, 'distance_accuracy_value', 'NONE');
#49424=CARTESIAN_POINT ( 'NONE',  ( -10.38582326156070046, 145.0440906288519898, 0.000000000000000000 ) ) ;
#49494=CARTESIAN_POINT ( 'NONE',  ( -4.313246244820144959, 141.0138720982649829, 5.000000000000002665 ) ) ;
#49553=COLOUR_RGB ( '', 0.66274510, 0.83137255, 0.94901961) ;
#49578=TOROIDAL_SURFACE ( 'NONE', #106392, 7.500000000000000888, 5.000000000000000000 ) ;
#49737=CARTESIAN_POINT ( 'NONE',  ( 7.869432500664373720, 87.30546385994320246, 5.000000000000000888 ) ) ;
#49805=CARTESIAN_POINT ( 'NONE',  ( -4.403431911294753753, 10.10497258083900363, -5.000000000000000000 ) ) ;
#49807=( NAMED_UNIT ( * ) PLANE_ANGLE_UNIT ( ) SI_UNIT ( $, .RADIAN. ) );
#49888=CIRCLE ( 'NONE', #63704, 7.500000000000000888 ) ;
#50016=DIRECTION ( 'NONE',  ( -0.1659550938513554008, -0.9861333108788019608, 5.358985056532664480E-15 ) ) ;
#50095=B_SPLINE_CURVE_WITH_KNOTS ( 'NONE', 3,
 ( #86731, #11736, #12805, #78601, #94279, #53285, #86206, #12278, #24133, #16004, #14926, #65621, #65082, #38704, #73152, #7897, #31161, #105540, #55897, #106599 ),
 .UNSPECIFIED., .F., .F.,
 ( 4, 2, 2, 2, 2, 2, 2, 2, 2, 4 ),
 ( -6.890858614811975829E-05, 0.0009161940774506751629, 0.001901296741049470071, 0.002886399404648264978, 0.003871502068247059669, 0.004856604731845854360, 0.005841707395444649918, 0.006334258727244045963, 0.006826810059043442007, 0.007811912722642235830 ),
 .UNSPECIFIED. ) ;
#50177=PRESENTATION_STYLE_ASSIGNMENT (( #17305 ) ) ;
#50254=SURFACE_STYLE_FILL_AREA ( #17380 ) ;
#50284=CARTESIAN_POINT ( 'NONE',  ( -5.000000000000002665, 152.0000000000000000, 5.000000000000000000 ) ) ;
#50304=CARTESIAN_POINT ( 'NONE',  ( -5.832992532897281812, 4.736036812732102419, -5.000000000000000000 ) ) ;
#50355=ORIENTED_EDGE ( 'NONE', *, *, #69207, .F. ) ;
#50454=AXIS2_PLACEMENT_3D ( 'NONE', #7952, #24185, #83978 ) ;
#50458=SURFACE_STYLE_USAGE ( .BOTH. , #84977 ) ;
#50542=SURFACE_SIDE_STYLE ('',( #40878 ) ) ;
#50612=SURFACE_STYLE_USAGE ( .BOTH. , #17756 ) ;
#50788=( GEOMETRIC_REPRESENTATION_CONTEXT ( 3 ) GLOBAL_UNCERTAINTY_ASSIGNED_CONTEXT ( ( #51955 ) ) GLOBAL_UNIT_ASSIGNED_CONTEXT ( ( #52994, #52442, #76190 ) ) REPRESENTATION_CONTEXT ( 'NONE', 'WORKASPACE' ) );
#50824=CARTESIAN_POINT ( 'NONE',  ( -10.32854822922020332, 7.030784501320459512, 0.000000000000000000 ) ) ;
#50945=STYLED_ITEM ( 'NONE', ( #54169 ), #36583 ) ;
#51076=CARTESIAN_POINT ( 'NONE',  ( -8.474746145538347264, 26.96279221873305332, 4.999999999998729017 ) ) ;
#51084=ADVANCED_BREP_SHAPE_REPRESENTATION ( '', ( #55083, #10728 ), #2257 ) ;
#51126=ORIENTED_EDGE ( 'NONE', *, *, #30704, .F. ) ;
#51220=EDGE_LOOP ( 'NONE', ( #26459, #70159, #67045, #54326 ) ) ;
#51249=EDGE_LOOP ( 'NONE', ( #96010, #94520, #24114, #66213 ) ) ;
#51366=CARTESIAN_POINT ( 'NONE',  ( -10.16823181764050688, 7.259740064965972905, -5.000000000000079936 ) ) ;
#51380=CARTESIAN_POINT ( 'NONE',  ( 0.000000000000000000, 0.000000000000000000, 0.000000000000000000 ) ) ;
#51384=ORIENTED_EDGE ( 'NONE', *, *, #5792, .F. ) ;
#51401=( NAMED_UNIT ( * ) SI_UNIT ( $, .STERADIAN. ) SOLID_ANGLE_UNIT ( ) );
#51615=MECHANICAL_DESIGN_GEOMETRIC_PRESENTATION_REPRESENTATION('',(#67182),#24173);
#51621=CARTESIAN_POINT ( 'NONE',  ( -8.420453562163482175, 123.3148673108831872, 5.000000000001271871 ) ) ;
#51694=PRESENTATION_STYLE_ASSIGNMENT (( #50612 ) ) ;
#51722=CARTESIAN_POINT ( 'NONE',  ( 8.224467148767693914, 115.5412973725991748, 0.000000000000000000 ) ) ;
#51787=LINE ( 'NONE', #85229, #80430 ) ;
#51899=CARTESIAN_POINT ( 'NONE',  ( -10.43542583693917969, 6.878147458890213173, -5.000000000000404121 ) ) ;
#51924=AXIS2_PLACEMENT_3D ( 'NONE', #78229, #5919, #28658 ) ;
#51955=UNCERTAINTY_MEASURE_WITH_UNIT (LENGTH_MEASURE( 1.000000000000000082E-05 ), #52994, 'distance_accuracy_value', 'NONE');
#52048=DIRECTION ( 'NONE',  ( -0.000000000000000000, -0.000000000000000000, 1.000000000000000000 ) ) ;
#52111=DIRECTION ( 'NONE',  ( 0.1659550938513567886, -0.9861333108788017388, 8.636585917856486324E-17 ) ) ;
#52152=CARTESIAN_POINT ( 'NONE',  ( -7.939583658491363494, 97.05573068114591706, 0.000000000000000000 ) ) ;
#52191=AXIS2_PLACEMENT_3D ( 'NONE', #87793, #29587, #86744 ) ;
#52254=CARTESIAN_POINT ( 'NONE',  ( 8.020865862490420994, 47.74483808550569819, 5.000000000002456702 ) ) ;
#52305=COLOUR_RGB ( '', 0.66274510, 0.83137255, 0.94901961) ;
#52356=( LENGTH_UNIT ( ) NAMED_UNIT ( * ) SI_UNIT ( .MILLI., .METRE. ) );
#52427=CARTESIAN_POINT ( 'NONE',  ( -5.897136329696558654, 4.642285597044319978, -5.000000000000000000 ) ) ;
#52442=( NAMED_UNIT ( * ) PLANE_ANGLE_UNIT ( ) SI_UNIT ( $, .RADIAN. ) );
#52457=CARTESIAN_POINT ( 'NONE',  ( 7.869427812660441113, 87.30462500882723020, -5.000000000000000888 ) ) ;
#52626=FACE_OUTER_BOUND ( 'NONE', #13663, .T. ) ;
#52642=ORIENTED_EDGE ( 'NONE', *, *, #10190, .F. ) ;
#52681=CARTESIAN_POINT ( 'NONE',  ( -8.971954110182338127, 136.3305255230980606, 4.999999999999998224 ) ) ;
#52719=CIRCLE ( 'NONE', #61369, 7.500000000000000888 ) ;
#52727=MECHANICAL_DESIGN_GEOMETRIC_PRESENTATION_REPRESENTATION('',(#50945),#102708);
#52733=STYLED_ITEM ( 'NONE', ( #50177 ), #14716 ) ;
#52793=CARTESIAN_POINT ( 'NONE',  ( 8.986804597297368247, 136.5680015418640778, 4.999999999999385381 ) ) ;
#52868=( NAMED_UNIT ( * ) PLANE_ANGLE_UNIT ( ) SI_UNIT ( $, .RADIAN. ) );
#52869=ORIENTED_EDGE ( 'NONE', *, *, #34582, .F. ) ;
#52906=CARTESIAN_POINT ( 'NONE',  ( -8.613443109969679767, 128.9903607843504005, -5.777789833161706683E-31 ) ) ;
#52915=VERTEX_POINT ( 'NONE', #1914 ) ;
#52943=DIRECTION ( 'NONE',  ( 0.000000000000000000, 0.000000000000000000, -1.000000000000000000 ) ) ;
#52975=CARTESIAN_POINT ( 'NONE',  ( -9.421434414708310001, 10.25265380211026667, -5.000000000000000000 ) ) ;
#52994=( LENGTH_UNIT ( ) NAMED_UNIT ( * ) SI_UNIT ( .MILLI., .METRE. ) );
#53004=CARTESIAN_POINT ( 'NONE',  ( 8.763392006746210328, 132.4000990056190403, 0.000000000000000000 ) ) ;
#53046=EDGE_LOOP ( 'NONE', ( #5692, #44422, #93329, #72022 ) ) ;
#53200=CIRCLE ( 'NONE', #85927, 7.500000000000006217 ) ;
#53217=DIRECTION ( 'NONE',  ( -0.9861333108787085910, 0.1659550938519105401, 0.000000000000000000 ) ) ;
#53220=ORIENTED_EDGE ( 'NONE', *, *, #97880, .T. ) ;
#53233=CARTESIAN_POINT ( 'NONE',  ( -8.623093486246707684, 129.1228760232886259, 6.361996342910116291E-13 ) ) ;
#53285=CARTESIAN_POINT ( 'NONE',  ( -7.748892321275496542, 5.864906519858121392, -4.492850722662553586 ) ) ;
#53372=PRESENTATION_STYLE_ASSIGNMENT (( #12363 ) ) ;
#53411=SURFACE_SIDE_STYLE ('',( #60980 ) ) ;
#53437=SURFACE_SIDE_STYLE ('',( #103571 ) ) ;
#53508=CARTESIAN_POINT ( 'NONE',  ( -9.875464621210269911, 7.754124811870932277, 0.000000000000000000 ) ) ;
#53533=CARTESIAN_POINT ( 'NONE',  ( -4.250302202869334245, 140.3077797975455212, -4.999999999999999112 ) ) ;
#53534=CARTESIAN_POINT ( 'NONE',  ( 3.168323364912392748, 112.8168162893846329, -5.000000000000000000 ) ) ;
#53552=ORIENTED_EDGE ( 'NONE', *, *, #2710, .F. ) ;
#53602=ORIENTED_EDGE ( 'NONE', *, *, #64247, .F. ) ;
#53642=PRODUCT ( '6. Link', '6. Link', '', ( #97788 ) ) ;
#53719=COLOUR_RGB ( '', 0.66274510, 0.83137255, 0.94901961) ;
#53753=CARTESIAN_POINT ( 'NONE',  ( -5.891808878741445099, 4.649940788608668107, 4.999999999999999112 ) ) ;
#53791=AXIS2_PLACEMENT_3D ( 'NONE', #46168, #21913, #5177 ) ;
#53832=VERTEX_POINT ( 'NONE', #101319 ) ;
#53858=CARTESIAN_POINT ( 'NONE',  ( -3.983822489248328047, 136.6779593738534118, 4.999999999999998224 ) ) ;
#53945=CARTESIAN_POINT ( 'NONE',  ( -8.011504011031322037, 103.5457333638258604, 1.027162637006525905E-30 ) ) ;
#54011=CARTESIAN_POINT ( 'NONE',  ( -9.460558175875586784, 9.928212646478041137, 0.000000000000000000 ) ) ;
#54035=CARTESIAN_POINT ( 'NONE',  ( -2.845103660799776613, 79.93183047064682967, -4.999999999999998224 ) ) ;
#54055=AXIS2_PLACEMENT_3D ( 'NONE', #19705, #14065, #95535 ) ;
#54077=EDGE_CURVE ( 'NONE', #104064, #104530, #84934, .T. ) ;
#54110=AXIS2_PLACEMENT_3D ( 'NONE', #25972, #84161, #85219 ) ;
#54169=PRESENTATION_STYLE_ASSIGNMENT (( #104876 ) ) ;
#54257=CARTESIAN_POINT ( 'NONE',  ( -9.993721417938997931, 7.509139500188190652, 0.000000000000000000 ) ) ;
#54296=ORIENTED_EDGE ( 'NONE', *, *, #36439, .T. ) ;
#54322=AXIS2_PLACEMENT_3D ( 'NONE', #98499, #16527, #104473 ) ;
#54326=ORIENTED_EDGE ( 'NONE', *, *, #57418, .F. ) ;
#54361=CARTESIAN_POINT ( 'NONE',  ( -3.794355794024275585, 18.81003929889839554, 5.000000000000000000 ) ) ;
#54455=PRESENTATION_STYLE_ASSIGNMENT (( #63119 ) ) ;
#54457=CARTESIAN_POINT ( 'NONE',  ( -9.144505990959208575, 13.07246590495299721, 1.301042606982603743E-15 ) ) ;
#54495=CARTESIAN_POINT ( 'NONE',  ( -6.231493956936419387, 147.8264543773111654, -5.000000000000000000 ) ) ;
#54506=CARTESIAN_POINT ( 'NONE',  ( 8.959992805873426391, 136.1288340877951839, -1.733336949948533988E-30 ) ) ;
#54533=CARTESIAN_POINT ( 'NONE',  ( -9.875464623904795403, 7.754124812996235683, -5.000000000000000000 ) ) ;
#54552=AXIS2_PLACEMENT_3D ( 'NONE', #106180, #47948, #14514 ) ;
#54567=CARTESIAN_POINT ( 'NONE',  ( -3.208653136615946977, 114.8595236971249705, -4.999999999999998224 ) ) ;
#54568=CARTESIAN_POINT ( 'NONE',  ( 3.363266691732269109, 121.3108357054893958, -5.000000000000000000 ) ) ;
#54620=ORIENTED_EDGE ( 'NONE', *, *, #16070, .T. ) ;
#54694=ADVANCED_FACE ( 'NONE', ( #21430 ), #30580, .F. ) ;
#54745=CARTESIAN_POINT ( 'NONE',  ( 14.54015256618498242, 142.2617268803927288, 0.000000000000000000 ) ) ;
#54753=DIRECTION ( 'NONE',  ( -1.224646799147353207E-16, 1.000000000000000000, 0.000000000000000000 ) ) ;
#54797=CARTESIAN_POINT ( 'NONE',  ( -8.757836645904029993, 19.71581191399078037, -6.344007692567969030E-13 ) ) ;
#54839=SURFACE_SIDE_STYLE ('',( #39744 ) ) ;
#54909=CARTESIAN_POINT ( 'NONE',  ( -2.845099737707079246, 79.92971061019304102, 5.000000000000000000 ) ) ;
#54924=AXIS2_PLACEMENT_3D ( 'NONE', #64779, #90646, #73914 ) ;
#54952=DIRECTION ( 'NONE',  ( -0.000000000000000000, -0.000000000000000000, 1.000000000000000000 ) ) ;
#54994=FILL_AREA_STYLE_COLOUR ( '', #36444 ) ;
#55036=CARTESIAN_POINT ( 'NONE',  ( -7.500000000000001776, 0.000000000000000000, 5.000000000000000000 ) ) ;
#55045=STYLED_ITEM ( 'NONE', ( #54455 ), #32445 ) ;
#55048=CARTESIAN_POINT ( 'NONE',  ( 8.350192200756456629, 120.7540425153082424, -0.000000000000000000 ) ) ;
#55073=CARTESIAN_POINT ( 'NONE',  ( -3.309912378723064652, 32.69790338586646072, -5.000000000000000000 ) ) ;
#55083=MANIFOLD_SOLID_BREP ( 'Fillet1', #46316 ) ;
#55084=( NAMED_UNIT ( * ) PLANE_ANGLE_UNIT ( ) SI_UNIT ( $, .RADIAN. ) );
#55103=CARTESIAN_POINT ( 'NONE',  ( 9.075140000865630441, 14.05259049545391115, -5.000000000000000888 ) ) ;
#55164=CARTESIAN_POINT ( 'NONE',  ( 8.224453817188688731, 36.45934599358540140, 5.000000000000000888 ) ) ;
#55188=( LENGTH_UNIT ( ) NAMED_UNIT ( * ) SI_UNIT ( .MILLI., .METRE. ) );
#55210=CARTESIAN_POINT ( 'NONE',  ( 5.000000000000000888, 6.123233995736767268E-16, -5.000000000000000000 ) ) ;
#55290=EDGE_CURVE ( 'NONE', #12734, #12822, #727, .T. ) ;
#55300=VERTEX_POINT ( 'NONE', #43172 ) ;
#55327=CARTESIAN_POINT ( 'NONE',  ( -4.091067340831425092, 13.63436032547001631, 4.999999999999999112 ) ) ;
#55368=FILL_AREA_STYLE_COLOUR ( '', #9229 ) ;
#55373=( LENGTH_UNIT ( ) NAMED_UNIT ( * ) SI_UNIT ( .MILLI., .METRE. ) );
#55481=ORIENTED_EDGE ( 'NONE', *, *, #63842, .F. ) ;
#55516=FILL_AREA_STYLE ('',( #54994 ) ) ;
#55527=UNCERTAINTY_MEASURE_WITH_UNIT (LENGTH_MEASURE( 1.000000000000000082E-05 ), #17837, 'distance_accuracy_value', 'NONE');
#55560=DIRECTION ( 'NONE',  ( -1.000000000000000000, 0.000000000000000000, 0.000000000000000000 ) ) ;
#55593=CARTESIAN_POINT ( 'NONE',  ( -9.514962460608897388, 142.5298273665900979, -4.999999999999041655 ) ) ;
#55609=DIRECTION ( 'NONE',  ( -1.000000000000000000, 0.000000000000000000, 0.000000000000000000 ) ) ;
#55621=CARTESIAN_POINT ( 'NONE',  ( 4.678819457397442427, 8.078722181090824961, -5.000000000000000000 ) ) ;
#55682=CARTESIAN_POINT ( 'NONE',  ( 3.168323364909926720, 39.18318371059633876, 5.000000000000000000 ) ) ;
#55705=( NAMED_UNIT ( * ) PLANE_ANGLE_UNIT ( ) SI_UNIT ( $, .RADIAN. ) );
#55840=CARTESIAN_POINT ( 'NONE',  ( -9.996167984597942535, 7.505519767266282116, 0.000000000000000000 ) ) ;
#55884=CARTESIAN_POINT ( 'NONE',  ( 4.678819457397416670, 143.9212778189090614, -5.000000000000000000 ) ) ;
#55897=CARTESIAN_POINT ( 'NONE',  ( -10.00000000000000000, 7.499999999999984901, -0.3301471707461320904 ) ) ;
#56021=ORIENTED_EDGE ( 'NONE', *, *, #54077, .T. ) ;
#56118=CARTESIAN_POINT ( 'NONE',  ( -9.291918545757502201, 140.5484994665301599, 0.000000000000000000 ) ) ;
#56160=TOROIDAL_SURFACE ( 'NONE', #49251, 7.500000000000000888, 5.000000000000000000 ) ;
#56210=( LENGTH_UNIT ( ) NAMED_UNIT ( * ) SI_UNIT ( .MILLI., .METRE. ) );
#56328=CIRCLE ( 'NONE', #54552, 5.000000000000000888 ) ;
#56378=CARTESIAN_POINT ( 'NONE',  ( -9.999733828778108347, 7.500380388546896704, 5.000000000000000888 ) ) ;
#56513=FACE_OUTER_BOUND ( 'NONE', #64456, .T. ) ;
#56651=ORIENTED_EDGE ( 'NONE', *, *, #2698, .T. ) ;
#56654=DIRECTION ( 'NONE',  ( 0.000000000000000000, 0.000000000000000000, -1.000000000000000000 ) ) ;
#56751=ORIENTED_EDGE ( 'NONE', *, *, #36439, .F. ) ;
#56755=CARTESIAN_POINT ( 'NONE',  ( 9.609486011791082305, 8.908497650349785246, 0.000000000000000000 ) ) ;
#56878=VERTEX_POINT ( 'NONE', #103421 ) ;
#56902=ADVANCED_FACE ( 'NONE', ( #73692, #80189, #72634 ), #16000, .T. ) ;
#56914=CARTESIAN_POINT ( 'NONE',  ( -6.067394940365958611, 4.399108099114772408, 5.000000000000000888 ) ) ;
#57000=ORIENTED_EDGE ( 'NONE', *, *, #15030, .F. ) ;
#57030=CARTESIAN_POINT ( 'NONE',  ( -4.484401894551007572, 9.375573132718574954, 5.000000000000000888 ) ) ;
#57033=DIRECTION ( 'NONE',  ( 0.000000000000000000, 0.000000000000000000, 1.000000000000000000 ) ) ;
#57044=CARTESIAN_POINT ( 'NONE',  ( -9.433863490721467571, 141.8798491995649442, -6.333282113655117596E-13 ) ) ;
#57047=CIRCLE ( 'NONE', #65691, 5.000000000000002665 ) ;
#57126=UNCERTAINTY_MEASURE_WITH_UNIT (LENGTH_MEASURE( 1.000000000000000082E-05 ), #84072, 'distance_accuracy_value', 'NONE');
#57194=CARTESIAN_POINT ( 'NONE',  ( -3.981297741196698770, 136.6372954359305254, -5.000000000000002665 ) ) ;
#57225=CARTESIAN_POINT ( 'NONE',  ( 9.300689190521341132, 11.36225021108674405, -3.068995344595356157E-13 ) ) ;
#57283=CARTESIAN_POINT ( 'NONE',  ( 8.361452242971266102, 30.82456655884568519, 0.000000000000000000 ) ) ;
#57311=CARTESIAN_POINT ( 'NONE',  ( 4.561148568382666468, 143.2220574413671557, 5.000000000000000888 ) ) ;
#57418=EDGE_CURVE ( 'NONE', #98139, #56878, #40542, .T. ) ;
#57442=CARTESIAN_POINT ( 'NONE',  ( -6.425022312393147139, 3.888363280597711302, 5.000000000000000888 ) ) ;
#57554=CARTESIAN_POINT ( 'NONE',  ( -5.566314792736418937, 5.173014757752155468, 5.000000000000000000 ) ) ;
#57570=CARTESIAN_POINT ( 'NONE',  ( -9.514607632263416548, 142.5277189159678244, 4.999999999993908872 ) ) ;
#57723=CARTESIAN_POINT ( 'NONE',  ( -8.618528913615500997, 129.1314578644004598, 1.270215581529557045E-12 ) ) ;
#57806=CIRCLE ( 'NONE', #92214, 12.50000000000000000 ) ;
#57818=CARTESIAN_POINT ( 'NONE',  ( 8.441132293725070568, 123.9914807902447507, 4.999999999997543298 ) ) ;
#57825=EDGE_LOOP ( 'NONE', ( #22294, #17726, #83841, #87534 ) ) ;
#57840=CARTESIAN_POINT ( 'NONE',  ( 4.322797252088989239, 141.1113215272794434, 5.000000000000000000 ) ) ;
#57998=CARTESIAN_POINT ( 'NONE',  ( -7.983737360691460339, 6.035846803540888317, 4.337628496855524318 ) ) ;
#58032=CARTESIAN_POINT ( 'NONE',  ( 4.322797252088743214, 10.88867847272319977, -4.999999999999997335 ) ) ;
#58177=AXIS2_PLACEMENT_3D ( 'NONE', #42921, #2982, #101689 ) ;
#58222=CIRCLE ( 'NONE', #11705, 12.50000000000000533 ) ;
#58259=EDGE_CURVE ( 'NONE', #3260, #104530, #2022, .T. ) ;
#58349=FACE_OUTER_BOUND ( 'NONE', #3791, .T. ) ;
#58411=CARTESIAN_POINT ( 'NONE',  ( -9.998878006837353283, 7.501608443958052597, -5.000000000000000888 ) ) ;
#58435=CARTESIAN_POINT ( 'NONE',  ( -6.231493956936419387, 147.8264543773111654, 0.000000000000000000 ) ) ;
#58541=CARTESIAN_POINT ( 'NONE',  ( -10.00988628808512892, 7.485880917377090604, 0.000000000000000000 ) ) ;
#58556=CARTESIAN_POINT ( 'NONE',  ( -7.262644754617018528, 5.510625410730323637, 4.742616764343380531 ) ) ;
#58565=DIRECTION ( 'NONE',  ( -0.000000000000000000, -0.000000000000000000, 1.000000000000000000 ) ) ;
#58614=CARTESIAN_POINT ( 'NONE',  ( -7.500000000000006217, 152.0000000000000000, 0.000000000000000000 ) ) ;
#58616=SURFACE_STYLE_FILL_AREA ( #25758 ) ;
#58899=( LENGTH_UNIT ( ) NAMED_UNIT ( * ) SI_UNIT ( .MILLI., .METRE. ) );
#58925=ORIENTED_EDGE ( 'NONE', *, *, #87726, .T. ) ;
#58948=CARTESIAN_POINT ( 'NONE',  ( 0.000000000000000000, 0.000000000000000000, 0.000000000000000000 ) ) ;
#58975=DIRECTION ( 'NONE',  ( 0.8308658609248572580, 0.5564727496918387972, 0.000000000000000000 ) ) ;
#58979=CARTESIAN_POINT ( 'NONE',  ( -3.948926469565266828, 15.90677080288882905, -5.000000000000000888 ) ) ;
#59082=DIRECTION ( 'NONE',  ( 0.5564727496918402405, -0.8308658609248562588, -0.000000000000000000 ) ) ;
#59114=FILL_AREA_STYLE ('',( #9466 ) ) ;
#59185=DIRECTION ( 'NONE',  ( 0.000000000000000000, 0.000000000000000000, 1.000000000000000000 ) ) ;
#59204=CARTESIAN_POINT ( 'NONE',  ( -3.310848799520615504, 32.66010184960634888, 5.000000000000000000 ) ) ;
#59211=EDGE_CURVE ( 'NONE', #91113, #104064, #34457, .T. ) ;
#59222=CARTESIAN_POINT ( 'NONE',  ( -5.000000000000000888, 0.000000000000000000, 5.000000000000000000 ) ) ;
#59377=DIRECTION ( 'NONE',  ( -0.000000000000000000, -0.000000000000000000, -1.000000000000000000 ) ) ;
#59431=DIRECTION ( 'NONE',  ( 0.000000000000000000, 0.000000000000000000, -1.000000000000000000 ) ) ;
#59455=TOROIDAL_SURFACE ( 'NONE', #88692, 7.500000000000000888, 5.000000000000000000 ) ;
#59488=CARTESIAN_POINT ( 'NONE',  ( -9.993183759060100257, 7.509940706430752400, -5.000000000000000888 ) ) ;
#59646=SURFACE_STYLE_FILL_AREA ( #59114 ) ;
#59737=CARTESIAN_POINT ( 'NONE',  ( -8.241419208044183264, 35.69988999158558585, 0.000000000000000000 ) ) ;
#59849=CARTESIAN_POINT ( 'NONE',  ( 7.849086896556030979, 70.34805173277894141, 4.999999999997544187 ) ) ;
#60012=DIRECTION ( 'NONE',  ( 0.9861333108788017388, 0.1659550938513568163, 0.000000000000000000 ) ) ;
#60033=CARTESIAN_POINT ( 'NONE',  ( -5.603881765357392908, 5.085926155681621097, -5.000000000000000000 ) ) ;
#60060=CARTESIAN_POINT ( 'NONE',  ( -4.698741327953603886, 7.940184299454766226, -5.000000000000000888 ) ) ;
#60087=DIRECTION ( 'NONE',  ( -0.000000000000000000, -0.000000000000000000, 1.000000000000000000 ) ) ;
#60286=CARTESIAN_POINT ( 'NONE',  ( -2.860285599241079169, 85.38585347072158527, 5.000000000000000000 ) ) ;
#60369=DIRECTION ( 'NONE',  ( -1.000000000000000000, 0.000000000000000000, 0.000000000000000000 ) ) ;
#60383=CARTESIAN_POINT ( 'NONE',  ( 3.768877481699944632, 132.6348382055886646, 5.000000000000000888 ) ) ;
#60552=CIRCLE ( 'NONE', #1922, 5.000000000000002665 ) ;
#60554=SURFACE_STYLE_USAGE ( .BOTH. , #35772 ) ;
#60556=CARTESIAN_POINT ( 'NONE',  ( -9.998878006819809983, 7.501608443945841032, 0.000000000000000000 ) ) ;
#60670=MECHANICAL_DESIGN_GEOMETRIC_PRESENTATION_REPRESENTATION('',(#95071),#3758);
#60802=CARTESIAN_POINT ( 'NONE',  ( -8.002549191621405100, 102.8991202088225521, 5.000000000000000888 ) ) ;
#60906=CARTESIAN_POINT ( 'NONE',  ( 8.830661707065113220, 133.7962572603239551, 5.000000000000614619 ) ) ;
#60980=SURFACE_STYLE_FILL_AREA ( #78720 ) ;
#61011=DIRECTION ( 'NONE',  ( 0.000000000000000000, 0.000000000000000000, -1.000000000000000000 ) ) ;
#61014=CARTESIAN_POINT ( 'NONE',  ( -8.466070237930688691, 27.19802938155146421, 0.000000000000000000 ) ) ;
#61074=CARTESIAN_POINT ( 'NONE',  ( 0.000000000000000000, 152.0000000000000000, 5.000000000000000000 ) ) ;
#61080=CARTESIAN_POINT ( 'NONE',  ( -9.737904751879213450, 8.235624462056064132, 0.000000000000000000 ) ) ;
#61094=SURFACE_STYLE_USAGE ( .BOTH. , #102064 ) ;
#61105=CARTESIAN_POINT ( 'NONE',  ( -3.346174626192466306, 120.6797456782134503, -4.999999999999999112 ) ) ;
#61106=CARTESIAN_POINT ( 'NONE',  ( 7.849089830965373160, 70.34685271985473776, -2.456708681988599773E-12 ) ) ;
#61108=DIRECTION ( 'NONE',  ( -1.224646799147353207E-16, 1.000000000000000000, 0.000000000000000000 ) ) ;
#61174=VERTEX_POINT ( 'NONE', #15870 ) ;
#61335=CARTESIAN_POINT ( 'NONE',  ( -7.844366129632167173, 79.51894426619178091, 5.000000000000000000 ) ) ;
#61369=AXIS2_PLACEMENT_3D ( 'NONE', #90930, #58565, #66107 ) ;
#61441=CARTESIAN_POINT ( 'NONE',  ( 8.020869781892258743, 104.2554943876434805, 5.000000000002456702 ) ) ;
#61497=CARTESIAN_POINT ( 'NONE',  ( 4.678819457397886517, 143.9212778189118467, 5.000000000000000000 ) ) ;
#61548=FILL_AREA_STYLE_COLOUR ( '', #41276 ) ;
#61624=CARTESIAN_POINT ( 'NONE',  ( -7.883628181806170865, 62.00818940277061841, 0.000000000000000000 ) ) ;
#61653=CARTESIAN_POINT ( 'NONE',  ( -3.227719910292865091, 36.27072058310572089, -5.000000000000000000 ) ) ;
#61654=CARTESIAN_POINT ( 'NONE',  ( 8.224453817208788209, 115.5406540063851679, 0.000000000000000000 ) ) ;
#61737=CARTESIAN_POINT ( 'NONE',  ( 3.168307535684220966, 39.18401492176337797, 5.000000000000000888 ) ) ;
#61757=ORIENTED_EDGE ( 'NONE', *, *, #9891, .F. ) ;
#61852=STYLED_ITEM ( 'NONE', ( #53372 ), #39853 ) ;
#61877=CARTESIAN_POINT ( 'NONE',  ( -9.692620405224255720, 8.443756516856183225, 0.000000000000000000 ) ) ;
#62143=CARTESIAN_POINT ( 'NONE',  ( 6.231493956936414058, 147.8264543773111654, 0.000000000000000000 ) ) ;
#62154=CARTESIAN_POINT ( 'NONE',  ( -9.590509843993705985, 9.008796699721322909, 0.000000000000000000 ) ) ;
#62164=( LENGTH_UNIT ( ) NAMED_UNIT ( * ) SI_UNIT ( .MILLI., .METRE. ) );
#62186=CARTESIAN_POINT ( 'NONE',  ( 9.300358455351362963, 140.6343319111669246, -4.999999999999999112 ) ) ;
#62239=( NAMED_UNIT ( * ) SI_UNIT ( $, .STERADIAN. ) SOLID_ANGLE_UNIT ( ) );
#62308=SURFACE_STYLE_FILL_AREA ( #103285 ) ;
#62345=CARTESIAN_POINT ( 'NONE',  ( 14.54015256618498242, 142.2617268803927288, 0.000000000000000000 ) ) ;
#62394=CARTESIAN_POINT ( 'NONE',  ( -9.880470759316240859, 7.740809967772715794, 0.000000000000000000 ) ) ;
#62501=CARTESIAN_POINT ( 'NONE',  ( -4.678819457397884740, 143.9212778189118467, 5.000000000000000000 ) ) ;
#62506=CARTESIAN_POINT ( 'NONE',  ( 0.000000000000000000, 152.0000000000000000, 5.000000000000000000 ) ) ;
#62540=( NAMED_UNIT ( * ) SI_UNIT ( $, .STERADIAN. ) SOLID_ANGLE_UNIT ( ) );
#62598=CARTESIAN_POINT ( 'NONE',  ( -7.850999800289822694, 69.61084308864499803, -0.000000000000000000 ) ) ;
#62644=CARTESIAN_POINT ( 'NONE',  ( 9.046046032567931050, 14.47514906270266977, -5.777789833161669899E-31 ) ) ;
#62652=( NAMED_UNIT ( * ) PLANE_ANGLE_UNIT ( ) SI_UNIT ( $, .RADIAN. ) );
#62666=DIRECTION ( 'NONE',  ( -0.000000000000000000, -0.000000000000000000, 1.000000000000000000 ) ) ;
#62671=CARTESIAN_POINT ( 'NONE',  ( -8.240610721200784639, 35.73638292219641244, 0.000000000000000000 ) ) ;
#62697=CARTESIAN_POINT ( 'NONE',  ( -3.426421942082409799, 123.5896999595963166, -4.999999999999999112 ) ) ;
#62698=CARTESIAN_POINT ( 'NONE',  ( 3.591870599023079258, 128.3878650910794192, -5.000000000000000000 ) ) ;
#62722=CIRCLE ( 'NONE', #24852, 5.000000000000000000 ) ;
#62749=PRESENTATION_STYLE_ASSIGNMENT (( #65784 ) ) ;
#62836=CIRCLE ( 'NONE', #16312, 7.500000000000000888 ) ;
#62914=COLOUR_RGB ( '', 0.31764706, 0.68627451, 0.89019608) ;
#62924=CARTESIAN_POINT ( 'NONE',  ( -9.550648136318311998, 9.268430070310975211, 4.999999999999841904 ) ) ;
#62959=CARTESIAN_POINT ( 'NONE',  ( 3.757221660946452602, 132.6327945012824898, -5.000000000000000000 ) ) ;
#63067=COLOUR_RGB ( '', 0.40784314, 0.44705882, 0.49803922) ;
#63119=SURFACE_STYLE_USAGE ( .BOTH. , #53437 ) ;
#63122=CARTESIAN_POINT ( 'NONE',  ( -8.154214789436208477, 112.0280654573990802, -7.222237291452134449E-31 ) ) ;
#63199=CARTESIAN_POINT ( 'NONE',  ( -9.545014793119364072, 9.306529264687913638, 0.000000000000000000 ) ) ;
#63230=CARTESIAN_POINT ( 'NONE',  ( 7.955551520408266519, 53.39349112219676385, 2.456524630699382222E-12 ) ) ;
#63289=CARTESIAN_POINT ( 'NONE',  ( 8.361452242992072570, 30.82456655884618968, 5.000000000000000888 ) ) ;
#63413=( NAMED_UNIT ( * ) SI_UNIT ( $, .STERADIAN. ) SOLID_ANGLE_UNIT ( ) );
#63463=CARTESIAN_POINT ( 'NONE',  ( -8.988144951968882523, 15.40598489177414976, 4.999999999999999112 ) ) ;
#63500=SURFACE_STYLE_FILL_AREA ( #32194 ) ;
#63631=EDGE_LOOP ( 'NONE', ( #34473, #54620, #38698, #65783 ) ) ;
#63664=CARTESIAN_POINT ( 'NONE',  ( -9.948648081855438363, 7.573338139540490843, -0.000000000000000000 ) ) ;
#63704=AXIS2_PLACEMENT_3D ( 'NONE', #7303, #75774, #27811 ) ;
#63708=MECHANICAL_DESIGN_GEOMETRIC_PRESENTATION_REPRESENTATION('',(#55045),#91276);
#63760=CARTESIAN_POINT ( 'NONE',  ( 9.439578325717800311, 10.07476781602096239, 3.068995344595395032E-13 ) ) ;
#63822=CARTESIAN_POINT ( 'NONE',  ( 9.609486011791082305, 8.908497650349785246, 5.000000000000000888 ) ) ;
#63823=DIRECTION ( 'NONE',  ( -1.000000000000000000, 0.000000000000000000, 0.000000000000000000 ) ) ;
#63842=EDGE_CURVE ( 'NONE', #30328, #56878, #16530, .T. ) ;
#63847=CARTESIAN_POINT ( 'NONE',  ( 3.168296453696582748, 112.8154174887550880, 5.000000000000000000 ) ) ;
#63945=CIRCLE ( 'NONE', #94893, 7.500000000000006217 ) ;
#63992=CYLINDRICAL_SURFACE ( 'NONE', #32724, 5.000000000000000888 ) ;
#63994=CARTESIAN_POINT ( 'NONE',  ( -8.988144951836199326, 15.40598489176668551, -6.352460523676195047E-13 ) ) ;
#64103=CARTESIAN_POINT ( 'NONE',  ( -4.201585111823095353, 12.27236537274642991, 5.000000000000000888 ) ) ;
#64247=EDGE_CURVE ( 'NONE', #104530, #104064, #35588, .T. ) ;
#64262=CARTESIAN_POINT ( 'NONE',  ( -8.734619362451120139, 132.0311980842931519, -5.000000000000003553 ) ) ;
#64270=STYLED_ITEM ( 'NONE', ( #25245 ), #95259 ) ;
#64290=CARTESIAN_POINT ( 'NONE',  ( 4.561387878959841657, 8.776520571373385593, -5.000000000000000000 ) ) ;
#64345=EDGE_CURVE ( 'NONE', #1254, #97405, #47624, .T. ) ;
#64355=CARTESIAN_POINT ( 'NONE',  ( 9.439237903995151058, 10.07757316356634192, 5.000000000001538325 ) ) ;
#64456=EDGE_LOOP ( 'NONE', ( #36625, #6594, #53602, #28847 ) ) ;
#64530=CARTESIAN_POINT ( 'NONE',  ( -5.000000000000000888, 0.000000000000000000, -5.000000000000000000 ) ) ;
#64619=CARTESIAN_POINT ( 'NONE',  ( -4.699253986252788451, 7.937442318057748025, 5.000000000000000000 ) ) ;
#64778=CARTESIAN_POINT ( 'NONE',  ( -4.557400256674738692, 143.1997842995386634, -5.000000000000000000 ) ) ;
#64779=CARTESIAN_POINT ( 'NONE',  ( 14.54015256618498242, 142.2617268803927288, 5.000000000000000000 ) ) ;
#64806=CARTESIAN_POINT ( 'NONE',  ( 9.518114778801557208, 9.451441023734561853, -4.999999999999691802 ) ) ;
#64864=SURFACE_SIDE_STYLE ('',( #23914 ) ) ;
#64969=ORIENTED_EDGE ( 'NONE', *, *, #82052, .F. ) ;
#65023=CARTESIAN_POINT ( 'NONE',  ( -10.00988628808512182, 7.485880917377084387, 5.000000000000004441 ) ) ;
#65082=CARTESIAN_POINT ( 'NONE',  ( -9.590319992950549377, 7.202961444570311400, -2.216063517372654612 ) ) ;
#65084=CIRCLE ( 'NONE', #66870, 5.000000000000000888 ) ;
#65090=UNCERTAINTY_MEASURE_WITH_UNIT (LENGTH_MEASURE( 1.000000000000000082E-05 ), #7699, 'distance_accuracy_value', 'NONE');
#65103=ORIENTED_EDGE ( 'NONE', *, *, #64247, .T. ) ;
#65147=ORIENTED_EDGE ( 'NONE', *, *, #55290, .T. ) ;
#65150=FACE_OUTER_BOUND ( 'NONE', #39257, .T. ) ;
#65188=AXIS2_PLACEMENT_3D ( 'NONE', #34406, #1444, #100160 ) ;
#65310=CARTESIAN_POINT ( 'NONE',  ( -8.147310229349574939, 111.6670789908333745, -5.000000000003809397 ) ) ;
#65330=VERTEX_POINT ( 'NONE', #13555 ) ;
#65338=CARTESIAN_POINT ( 'NONE',  ( 3.768877481701073950, 19.36516179434251939, -5.000000000000000000 ) ) ;
#65558=CARTESIAN_POINT ( 'NONE',  ( -10.31642403553700404, 7.048099644362463501, 5.000000000000000888 ) ) ;
#65616=( NAMED_UNIT ( * ) SI_UNIT ( $, .STERADIAN. ) SOLID_ANGLE_UNIT ( ) );
#65621=CARTESIAN_POINT ( 'NONE',  ( -9.466116368847748319, 7.112870702781648902, -2.503129221841524199 ) ) ;
#65672=CARTESIAN_POINT ( 'NONE',  ( -4.640907980698733226, 8.296333112989275449, 5.000000000000000888 ) ) ;
#65691=AXIS2_PLACEMENT_3D ( 'NONE', #62506, #4261, #3197 ) ;
#65725=( GEOMETRIC_REPRESENTATION_CONTEXT ( 3 ) GLOBAL_UNCERTAINTY_ASSIGNED_CONTEXT ( ( #97062 ) ) GLOBAL_UNIT_ASSIGNED_CONTEXT ( ( #102514, #71709, #30228 ) ) REPRESENTATION_CONTEXT ( 'NONE', 'WORKASPACE' ) );
#65783=ORIENTED_EDGE ( 'NONE', *, *, #92450, .F. ) ;
#65784=SURFACE_STYLE_USAGE ( .BOTH. , #32907 ) ;
#65929=CARTESIAN_POINT ( 'NONE',  ( -7.500000000000006217, 152.0000000000000000, 0.000000000000000000 ) ) ;
#65930=CARTESIAN_POINT ( 'NONE',  ( 9.518114776852277359, 142.5485589766093710, 0.000000000000000000 ) ) ;
#65932=CARTESIAN_POINT ( 'NONE',  ( -6.231493956936421164, 147.8264543773111654, 0.000000000000000000 ) ) ;
#65966=PRESENTATION_STYLE_ASSIGNMENT (( #33101 ) ) ;
#66043=DIRECTION ( 'NONE',  ( -1.000000000000000000, 0.000000000000000000, 0.000000000000000000 ) ) ;
#66107=DIRECTION ( 'NONE',  ( -1.000000000000000000, 2.664535259100375697E-15, 0.000000000000000000 ) ) ;
#66150=UNCERTAINTY_MEASURE_WITH_UNIT (LENGTH_MEASURE( 1.000000000000000082E-05 ), #55188, 'distance_accuracy_value', 'NONE');
#66198=SURFACE_STYLE_USAGE ( .BOTH. , #33328 ) ;
#66213=ORIENTED_EDGE ( 'NONE', *, *, #86303, .F. ) ;
#66291=CARTESIAN_POINT ( 'NONE',  ( 0.000000000000000000, 0.000000000000000000, -5.000000000000000000 ) ) ;
#66493=CARTESIAN_POINT ( 'NONE',  ( -10.03463480799099550, 7.450536368003703558, -5.000000000000017764 ) ) ;
#66528=CARTESIAN_POINT ( 'NONE',  ( -4.036417550650834407, 14.45404279547049065, -5.000000000000000888 ) ) ;
#66578=( BOUNDED_SURFACE ( )  B_SPLINE_SURFACE ( 3, 2, ( 
 ( #70251, #4446, #104193 ),
 ( #86980, #77815, #44385 ),
 ( #103152, #103675, #37390 ),
 ( #93474, #62186, #19624 ),
 ( #13050, #20696, #28775 ),
 ( #45455, #102073, #29820 ),
 ( #11459, #28234, #69725 ),
 ( #29298, #44930, #71301 ),
 ( #53004, #102617, #95072 ),
 ( #37919, #45980, #4988 ),
 ( #36335, #77280, #62698 ),
 ( #95590, #21726, #78859 ),
 ( #70780, #30337, #54568 ),
 ( #61654, #79394, #20154 ),
 ( #46500, #87504, #53534 ),
 ( #94544, #85926, #86464 ),
 ( #13584, #36857, #5511 ),
 ( #38435, #52457, #12522 ),
 ( #85374, #3392, #69204 ),
 ( #61106, #11998, #78330 ),
 ( #14639, #82034, #88033 ),
 ( #63230, #96122, #31928 ),
 ( #105266, #89620, #97161 ),
 ( #6026, #15183, #71827 ),
 ( #48604, #14113, #104731 ),
 ( #8158, #72877, #47547 ),
 ( #98229, #22785, #72362 ),
 ( #96650, #7609, #15718 ),
 ( #89088, #38949, #47016 ),
 ( #48072, #32468, #65338 ),
 ( #39487, #105789, #73948 ),
 ( #22254, #40005, #24384 ),
 ( #40528, #55103, #6553 ),
 ( #31413, #88558, #80973 ),
 ( #57225, #30882, #23309 ),
 ( #63760, #90144, #16247 ),
 ( #97688, #64806, #64290 ),
 ( #79918, #23852, #55621 ) ),
 .UNSPECIFIED., .F., .F., .F. ) 
 B_SPLINE_SURFACE_WITH_KNOTS ( ( 4, 2, 2, 2, 2, 2, 2, 2, 2, 2, 2, 2, 2, 2, 2, 2, 2, 2, 4 ),
 ( 3, 3 ),
 ( 0.06375477930561496143, 0.06591736287010036000, 0.06807994643458575856, 0.07240511356355655570, 0.07673028069252735284, 0.08105544782149814997, 0.08970578207943974425, 0.09835611633738133852, 0.1156567848532645271, 0.1329574533691477156, 0.1502581218850309042, 0.1675587904009140927, 0.1762091246588556870, 0.1848594589167972813, 0.1891846260457680784, 0.1935097931747388755, 0.1978349603037096727, 0.1999975438681950712, 0.2021601274326804976 ),
 ( 0.000000000000000000, 1.000000000000000000 ),
 .UNSPECIFIED. ) 
 GEOMETRIC_REPRESENTATION_ITEM ( )  RATIONAL_B_SPLINE_SURFACE ( (
 ( 1.000000000000000000, 0.7071067811865475727, 1.000000000000000000),
 ( 1.000000000000000000, 0.7071067811865475727, 1.000000000000000000),
 ( 1.000000000000000000, 0.7071067811865475727, 1.000000000000000000),
 ( 1.000000000000000000, 0.7071067811865475727, 1.000000000000000000),
 ( 1.000000000000000000, 0.7071067811865475727, 1.000000000000000000),
 ( 1.000000000000000000, 0.7071067811865475727, 1.000000000000000000),
 ( 1.000000000000000000, 0.7071067811865475727, 1.000000000000000000),
 ( 1.000000000000000000, 0.7071067811865475727, 1.000000000000000000),
 ( 1.000000000000000000, 0.7071067811865475727, 1.000000000000000000),
 ( 1.000000000000000000, 0.7071067811865475727, 1.000000000000000000),
 ( 1.000000000000000000, 0.7071067811865474617, 1.000000000000000000),
 ( 1.000000000000000000, 0.7071067811865474617, 1.000000000000000000),
 ( 1.000000000000000000, 0.7071067811865474617, 1.000000000000000000),
 ( 1.000000000000000000, 0.7071067811865474617, 1.000000000000000000),
 ( 1.000000000000000000, 0.7071067811865475727, 1.000000000000000000),
 ( 1.000000000000000000, 0.7071067811865475727, 1.000000000000000000),
 ( 1.000000000000000000, 0.7071067811865475727, 1.000000000000000000),
 ( 1.000000000000000000, 0.7071067811865475727, 1.000000000000000000),
 ( 1.000000000000000000, 0.7071067811865475727, 1.000000000000000000),
 ( 1.000000000000000000, 0.7071067811865475727, 1.000000000000000000),
 ( 1.000000000000000000, 0.7071067811865475727, 1.000000000000000000),
 ( 1.000000000000000000, 0.7071067811865475727, 1.000000000000000000),
 ( 1.000000000000000000, 0.7071067811865475727, 1.000000000000000000),
 ( 1.000000000000000000, 0.7071067811865475727, 1.000000000000000000),
 ( 1.000000000000000000, 0.7071067811865475727, 1.000000000000000000),
 ( 1.000000000000000000, 0.7071067811865475727, 1.000000000000000000),
 ( 1.000000000000000000, 0.7071067811865475727, 1.000000000000000000),
 ( 1.000000000000000000, 0.7071067811865475727, 1.000000000000000000),
 ( 1.000000000000000000, 0.7071067811865475727, 1.000000000000000000),
 ( 1.000000000000000000, 0.7071067811865475727, 1.000000000000000000),
 ( 1.000000000000000000, 0.7071067811865475727, 1.000000000000000000),
 ( 1.000000000000000000, 0.7071067811865475727, 1.000000000000000000),
 ( 1.000000000000000000, 0.7071067811865475727, 1.000000000000000000),
 ( 1.000000000000000000, 0.7071067811865475727, 1.000000000000000000),
 ( 1.000000000000000000, 0.7071067811865475727, 1.000000000000000000),
 ( 1.000000000000000000, 0.7071067811865475727, 1.000000000000000000),
 ( 1.000000000000000000, 0.7071067811865475727, 1.000000000000000000),
 ( 1.000000000000000000, 0.7071067811865475727, 1.000000000000000000) ) ) 
 REPRESENTATION_ITEM ( '' )  SURFACE ( )  );
#66633=CARTESIAN_POINT ( 'NONE',  ( -6.088311765594377256, 4.652913962454959140, 5.000000000000019540 ) ) ;
#66705=CARTESIAN_POINT ( 'NONE',  ( -9.999999999999982236, 7.499999999999973355, 0.000000000000000000 ) ) ;
#66738=CARTESIAN_POINT ( 'NONE',  ( -5.128020333435169498, 6.165036831253548399, 5.000000000000001776 ) ) ;
#66750=AXIS2_PLACEMENT_3D ( 'NONE', #30272, #98160, #55560 ) ;
#66785=CARTESIAN_POINT ( 'NONE',  ( 7.500000000000006217, 152.0000000000000000, 0.000000000000000000 ) ) ;
#66832=DIRECTION ( 'NONE',  ( 0.000000000000000000, 0.000000000000000000, -1.000000000000000000 ) ) ;
#66849=ORIENTED_EDGE ( 'NONE', *, *, #47662, .F. ) ;
#66870=AXIS2_PLACEMENT_3D ( 'NONE', #25690, #59082, #33758 ) ;
#66986=( NAMED_UNIT ( * ) SI_UNIT ( $, .STERADIAN. ) SOLID_ANGLE_UNIT ( ) );
#67042=CARTESIAN_POINT ( 'NONE',  ( -6.446543223214487917, 3.857628234704938652, -5.000000000000000000 ) ) ;
#67045=ORIENTED_EDGE ( 'NONE', *, *, #104735, .F. ) ;
#67182=STYLED_ITEM ( 'NONE', ( #22954 ), #72138 ) ;
#67296=CARTESIAN_POINT ( 'NONE',  ( -8.309329435532722741, 32.78459446883342565, 5.000000000001270095 ) ) ;
#67368=FILL_AREA_STYLE_COLOUR ( '', #53719 ) ;
#67575=CARTESIAN_POINT ( 'NONE',  ( -9.995757844555885896, 7.506119843332723640, 0.000000000000000000 ) ) ;
#67739=CARTESIAN_POINT ( 'NONE',  ( 2.849088235197433594, 81.66451978571728887, -5.000000000000000000 ) ) ;
#67773=UNCERTAINTY_MEASURE_WITH_UNIT (LENGTH_MEASURE( 1.000000000000000082E-05 ), #35883, 'distance_accuracy_value', 'NONE');
#67818=CARTESIAN_POINT ( 'NONE',  ( -3.147946884150642610, 111.7483634657347551, 5.000000000000000000 ) ) ;
#67890=DIRECTION ( 'NONE',  ( -1.000000000000000000, 0.000000000000000000, 0.000000000000000000 ) ) ;
#67896=EDGE_CURVE ( 'NONE', #44531, #80759, #92661, .T. ) ;
#67907=DIRECTION ( 'NONE',  ( 0.000000000000000000, 0.000000000000000000, -1.000000000000000000 ) ) ;
#67918=CARTESIAN_POINT ( 'NONE',  ( 3.836994546497918268, 134.0493965400703189, 5.000000000000000888 ) ) ;
#67983=CARTESIAN_POINT ( 'NONE',  ( 0.000000000000000000, 0.000000000000000000, 5.000000000000000000 ) ) ;
#68092=CARTESIAN_POINT ( 'NONE',  ( -9.998567040921154003, 7.502056690377623127, -4.999999999999999112 ) ) ;
#68117=CARTESIAN_POINT ( 'NONE',  ( -5.850740358028501120, 4.708522909031559678, -4.999999999999999112 ) ) ;
#68124=DIRECTION ( 'NONE',  ( -1.000000000000000000, 0.000000000000000000, 0.000000000000000000 ) ) ;
#68138=ORIENTED_EDGE ( 'NONE', *, *, #67896, .F. ) ;
#68357=CARTESIAN_POINT ( 'NONE',  ( -3.981089209424774733, 136.6339151386011110, 4.999999999999997335 ) ) ;
#68421=DIRECTION ( 'NONE',  ( -1.000000000000000000, 0.000000000000000000, 0.000000000000000000 ) ) ;
#68425=ORIENTED_EDGE ( 'NONE', *, *, #82201, .T. ) ;
#68461=CARTESIAN_POINT ( 'NONE',  ( 8.588478090880302673, 128.2033481600901723, 5.000000000001228351 ) ) ;
#68610=CIRCLE ( 'NONE', #16930, 12.50000000000000533 ) ;
#68614=UNCERTAINTY_MEASURE_WITH_UNIT (LENGTH_MEASURE( 1.000000000000000082E-05 ), #56210, 'distance_accuracy_value', 'NONE');
#68648=CARTESIAN_POINT ( 'NONE',  ( -5.898801552711128160, 4.639897325518991700, -5.000000000000000000 ) ) ;
#68899=CARTESIAN_POINT ( 'NONE',  ( -3.626860598991949125, 129.3176399044602931, 5.000000000000000888 ) ) ;
#68999=CARTESIAN_POINT ( 'NONE',  ( 7.869427812660434896, 64.69537499111491741, 4.999999999992629895 ) ) ;
#69039=EDGE_LOOP ( 'NONE', ( #22967, #32860, #79173, #85145, #7186, #82103, #25888, #87233, #51384, #54296, #20473 ) ) ;
#69069=EDGE_LOOP ( 'NONE', ( #52642, #6019, #105157, #30204, #58925, #15519, #72145, #50355, #3040, #69523, #70102 ) ) ;
#69105=CARTESIAN_POINT ( 'NONE',  ( -9.341113524656639910, 10.95974597718367249, 1.301042606982605124E-15 ) ) ;
#69177=CARTESIAN_POINT ( 'NONE',  ( -4.498984042742175227, 9.307284623892885023, -5.000000000000000000 ) ) ;
#69204=CARTESIAN_POINT ( 'NONE',  ( 2.849086893379675356, 81.66418373412562914, -5.000000000000000000 ) ) ;
#69207=EDGE_CURVE ( 'NONE', #44531, #76218, #101447, .T. ) ;
#69424=CARTESIAN_POINT ( 'NONE',  ( -3.342287015225765767, 120.5339020451717289, 5.000000000000000000 ) ) ;
#69499=STYLED_ITEM ( 'NONE', ( #14173 ), #97466 ) ;
#69507=COLOUR_RGB ( '', 0.08235294, 0.09019608, 0.10196078) ;
#69522=CARTESIAN_POINT ( 'NONE',  ( 4.323075853814084546, 141.1141821973716617, 5.000000000000000888 ) ) ;
#69523=ORIENTED_EDGE ( 'NONE', *, *, #41428, .T. ) ;
#69629=CARTESIAN_POINT ( 'NONE',  ( -9.559480721551260274, 9.206076766727413485, -0.000000000000000000 ) ) ;
#69699=CARTESIAN_POINT ( 'NONE',  ( -9.248416039723647231, 11.93391985749765105, -3.173712385738878837E-13 ) ) ;
#69725=CARTESIAN_POINT ( 'NONE',  ( 3.996239228618861272, 136.8763022136764675, -4.999999999999999112 ) ) ;
#69829=CIRCLE ( 'NONE', #25033, 5.000000000000000888 ) ;
#69839=CARTESIAN_POINT ( 'NONE',  ( 0.000000000000000000, 152.0000000000000000, -5.000000000000000000 ) ) ;
#69890=UNCERTAINTY_MEASURE_WITH_UNIT (LENGTH_MEASURE( 1.000000000000000082E-05 ), #75813, 'distance_accuracy_value', 'NONE');
#69946=CARTESIAN_POINT ( 'NONE',  ( -4.272176768629773136, 11.44367718774164189, 4.999999999999999112 ) ) ;
#70048=CARTESIAN_POINT ( 'NONE',  ( -3.058406714429998896, 44.99895710957036954, 5.000000000000000000 ) ) ;
#70102=ORIENTED_EDGE ( 'NONE', *, *, #37906, .T. ) ;
#70153=CARTESIAN_POINT ( 'NONE',  ( -9.414516558252268297, 10.25650596040859774, 0.000000000000000000 ) ) ;
#70159=ORIENTED_EDGE ( 'NONE', *, *, #3881, .T. ) ;
#70207=SHAPE_REPRESENTATION ( '6. Link', ( #10728 ), #2257 ) ;
#70222=CARTESIAN_POINT ( 'NONE',  ( -3.994958879817047226, 15.13994505928113377, -5.000000000000000000 ) ) ;
#70244=CARTESIAN_POINT ( 'NONE',  ( 6.231493956936416723, 147.8264543773111654, 0.000000000000000000 ) ) ;
#70251=CARTESIAN_POINT ( 'NONE',  ( 9.609486011791064541, 143.0915023496501419, 0.000000000000000000 ) ) ;
#70256=DIRECTION ( 'NONE',  ( 0.000000000000000000, 0.000000000000000000, -1.000000000000000000 ) ) ;
#70300=CIRCLE ( 'NONE', #22042, 10.00000000000000000 ) ;
#70307=( NAMED_UNIT ( * ) PLANE_ANGLE_UNIT ( ) SI_UNIT ( $, .RADIAN. ) );
#70327=VERTEX_POINT ( 'NONE', #45060 ) ;
#70459=( GEOMETRIC_REPRESENTATION_CONTEXT ( 3 ) GLOBAL_UNCERTAINTY_ASSIGNED_CONTEXT ( ( #34414 ) ) GLOBAL_UNIT_ASSIGNED_CONTEXT ( ( #38276, #22083, #13951 ) ) REPRESENTATION_CONTEXT ( 'NONE', 'WORKASPACE' ) );
#70481=CARTESIAN_POINT ( 'NONE',  ( -9.971054622642887111, 7.543597282511679047, 0.000000000000000000 ) ) ;
#70574=TOROIDAL_SURFACE ( 'NONE', #24086, 10.00000000000000000, 5.000000000000000000 ) ;
#70626=SURFACE_STYLE_FILL_AREA ( #80823 ) ;
#70651=FILL_AREA_STYLE_COLOUR ( '', #141 ) ;
#70662=AXIS2_PLACEMENT_3D ( 'NONE', #61074, #62666, #11422 ) ;
#70712=ORIENTED_EDGE ( 'NONE', *, *, #76927, .T. ) ;
#70724=CARTESIAN_POINT ( 'NONE',  ( 9.269703125412263489, 140.3128462412892929, 1.540743955509799543E-30 ) ) ;
#70748=CARTESIAN_POINT ( 'NONE',  ( -3.573159493689508803, 23.91665737286602678, -5.000000000000000000 ) ) ;
#70763=DIRECTION ( 'NONE',  ( -0.000000000000000000, -0.000000000000000000, -1.000000000000000000 ) ) ;
#70780=CARTESIAN_POINT ( 'NONE',  ( 8.361452242971985527, 121.1754334411840830, 0.000000000000000000 ) ) ;
#70946=UNCERTAINTY_MEASURE_WITH_UNIT (LENGTH_MEASURE( 1.000000000000000082E-05 ), #38052, 'distance_accuracy_value', 'NONE');
#70997=CARTESIAN_POINT ( 'NONE',  ( -5.894985479084318136, 4.645370767574111603, 5.000000000000000000 ) ) ;
#71108=CARTESIAN_POINT ( 'NONE',  ( -4.314913995129422197, 141.0309651098860684, 5.000000000000000000 ) ) ;
#71148=FACE_OUTER_BOUND ( 'NONE', #32412, .T. ) ;
#71193=SURFACE_STYLE_FILL_AREA ( #55516 ) ;
#71199=CARTESIAN_POINT ( 'NONE',  ( -8.209867939952777860, 114.8553993246446652, 1.301042606982606307E-15 ) ) ;
#71271=CARTESIAN_POINT ( 'NONE',  ( -4.597609114482794190, 8.581307559369470539, -5.000000000000000000 ) ) ;
#71301=CARTESIAN_POINT ( 'NONE',  ( 3.836943873308563013, 134.0483964974777393, -4.999999999999999112 ) ) ;
#71356=CARTESIAN_POINT ( 'NONE',  ( 8.642223818518250056, 22.39656424817031422, 4.999999999999385381 ) ) ;
#71465=FILL_AREA_STYLE ('',( #88728 ) ) ;
#71517=CARTESIAN_POINT ( 'NONE',  ( -5.618500397171760419, 5.062260283225303859, 5.000000000000000888 ) ) ;
#71558=CARTESIAN_POINT ( 'NONE',  ( 2.955793532184392003, 98.65757386076514024, -5.000000000000000000 ) ) ;
#71566=SURFACE_STYLE_FILL_AREA ( #89889 ) ;
#71626=CARTESIAN_POINT ( 'NONE',  ( -2.983137620783093524, 50.82020749530228443, 5.000000000000000000 ) ) ;
#71709=( NAMED_UNIT ( * ) PLANE_ANGLE_UNIT ( ) SI_UNIT ( $, .RADIAN. ) );
#71762=CARTESIAN_POINT ( 'NONE',  ( 9.413036185852410753, 141.7043030661344858, -0.000000000000000000 ) ) ;
#71790=CARTESIAN_POINT ( 'NONE',  ( -7.860352320341752019, 85.38611325936935259, 5.079056458989159063E-12 ) ) ;
#71800=SURFACE_STYLE_FILL_AREA ( #78310 ) ;
#71827=CARTESIAN_POINT ( 'NONE',  ( 3.168333439190436529, 39.18265495645905361, -5.000000000000000000 ) ) ;
#71891=FILL_AREA_STYLE ('',( #98292 ) ) ;
#71906=EDGE_LOOP ( 'NONE', ( #84981, #101210, #33730, #99269 ) ) ;
#71918=( NAMED_UNIT ( * ) SI_UNIT ( $, .STERADIAN. ) SOLID_ANGLE_UNIT ( ) );
#71979=VECTOR ( 'NONE', #100736, 1000.000000000000000 ) ;
#72022=ORIENTED_EDGE ( 'NONE', *, *, #35413, .F. ) ;
#72059=CARTESIAN_POINT ( 'NONE',  ( -5.057453041531906557, 6.382334271672433168, 5.000000000000000000 ) ) ;
#72138=ADVANCED_FACE ( 'NONE', ( #29985 ), #70574, .T. ) ;
#72145=ORIENTED_EDGE ( 'NONE', *, *, #13911, .T. ) ;
#72171=CARTESIAN_POINT ( 'NONE',  ( -4.036663395287809486, 14.45006652701215977, 4.999999999999999112 ) ) ;
#72176=CARTESIAN_POINT ( 'NONE',  ( 0.000000000000000000, 152.0000000000000000, 5.000000000000000000 ) ) ;
#72207=STYLED_ITEM ( 'NONE', ( #62749 ), #102828 ) ;
#72307=CARTESIAN_POINT ( 'NONE',  ( 8.619428876659387839, 129.1420429763053903, -0.000000000000000000 ) ) ;
#72336=CARTESIAN_POINT ( 'NONE',  ( -9.514962458596817996, 142.5298273669549189, 0.000000000000000000 ) ) ;
#72362=CARTESIAN_POINT ( 'NONE',  ( 3.443379947491756354, 27.85683824479126258, -5.000000000000000000 ) ) ;
#72425=CARTESIAN_POINT ( 'NONE',  ( 9.517802784864830556, 9.453294932689157548, 9.300361635023031386E-13 ) ) ;
#72501=ORIENTED_EDGE ( 'NONE', *, *, #95117, .F. ) ;
#72511=CARTESIAN_POINT ( 'NONE',  ( -4.678819457397884740, 143.9212778189118467, 0.000000000000000000 ) ) ;
#72540=DIRECTION ( 'NONE',  ( -1.000000000000000000, -1.224646799147353207E-16, 0.000000000000000000 ) ) ;
#72543=ORIENTED_EDGE ( 'NONE', *, *, #37396, .F. ) ;
#72574=STYLED_ITEM ( 'NONE', ( #87925 ), #93079 ) ;
#72585=DIRECTION ( 'NONE',  ( -1.000000000000000000, 0.000000000000000000, 0.000000000000000000 ) ) ;
#72596=CARTESIAN_POINT ( 'NONE',  ( 0.000000000000000000, 152.0000000000000000, 5.000000000000000000 ) ) ;
#72625=DIRECTION ( 'NONE',  ( -1.000000000000000000, 0.000000000000000000, 0.000000000000000000 ) ) ;
#72634=FACE_BOUND ( 'NONE', #86224, .T. ) ;
#72681=B_SPLINE_CURVE_WITH_KNOTS ( 'NONE', 3,
 ( #55884, #73139, #87771, #6828, #48342, #23582, #89882, #62959, #95860, #13853, #46765, #79661, #104464, #38692, #71558, #42386, #67739, #75280, #83912, #74742, #293, #25731, #76343, #90959, #1918, #82314, #75822, #34870, #100625, #1375, #58032, #24643, #49409, #26787 ),
 .UNSPECIFIED., .F., .F.,
 ( 4, 2, 2, 2, 2, 2, 2, 2, 2, 2, 2, 2, 2, 2, 2, 2, 4 ),
 ( 0.000000000000000000, 0.002123632632474287216, 0.004247265264948574433, 0.008494530529897148866, 0.01698906105979429426, 0.02548359158969144139, 0.03397812211958858852, 0.05096718317938292442, 0.06795624423917726031, 0.08494530529897158233, 0.1019343663587659321, 0.1104288968886631278, 0.1189234274185603096, 0.1274179579484575053, 0.1316652232134060962, 0.1337888558458803778, 0.1359124884783546594 ),
 .UNSPECIFIED. ) ;
#72693=( NAMED_UNIT ( * ) PLANE_ANGLE_UNIT ( ) SI_UNIT ( $, .RADIAN. ) );
#72825=ORIENTED_EDGE ( 'NONE', *, *, #105352, .F. ) ;
#72844=CARTESIAN_POINT ( 'NONE',  ( -9.434261306993260376, 141.8831429913814759, -5.000000000000000888 ) ) ;
#72853=AXIS2_PLACEMENT_3D ( 'NONE', #4257, #37726, #22051 ) ;
#72877=CARTESIAN_POINT ( 'NONE',  ( 8.361479372609258220, 30.82354577482384173, -4.999999999999998224 ) ) ;
#72938=CARTESIAN_POINT ( 'NONE',  ( 4.086459164111219344, 13.71066660893832712, 5.000000000000000000 ) ) ;
#72964=CARTESIAN_POINT ( 'NONE',  ( 3.443309072005628746, 124.1408101220383600, 5.000000000000000000 ) ) ;
#73135=FILL_AREA_STYLE ('',( #55368 ) ) ;
#73139=CARTESIAN_POINT ( 'NONE',  ( 4.560915367935560738, 143.2206717247628944, -4.999999999999999112 ) ) ;
#73152=CARTESIAN_POINT ( 'NONE',  ( -9.787739683274441660, 7.346124691387062811, -1.606086870082999107 ) ) ;
#73203=CIRCLE ( 'NONE', #40493, 4.999999999999999112 ) ;
#73206=CIRCLE ( 'NONE', #31893, 7.500000000000000888 ) ;
#73249=DIRECTION ( 'NONE',  ( -1.000000000000000000, 0.000000000000000000, 0.000000000000000000 ) ) ;
#73264=MECHANICAL_DESIGN_GEOMETRIC_PRESENTATION_REPRESENTATION('',(#97376),#100843);
#73374=CARTESIAN_POINT ( 'NONE',  ( -7.860352320337314680, 85.38611325940999563, -4.999999999992382982 ) ) ;
#73632=CARTESIAN_POINT ( 'NONE',  ( -5.920512269712092213, 4.608878292434047452, 5.000000000000000888 ) ) ;
#73646=CARTESIAN_POINT ( 'NONE',  ( -9.466035365373274502, 7.112811939922738524, 2.503306211807451831 ) ) ;
#73668=COLOUR_RGB ( '', 0.31764706, 0.68627451, 0.89019608) ;
#73692=FACE_OUTER_BOUND ( 'NONE', #69039, .T. ) ;
#73913=CARTESIAN_POINT ( 'NONE',  ( -9.061861678394784292, 137.7616487646406256, -5.000000000000000888 ) ) ;
#73914=DIRECTION ( 'NONE',  ( -1.000000000000000000, 2.498001805406602216E-14, 0.000000000000000000 ) ) ;
#73948=CARTESIAN_POINT ( 'NONE',  ( 3.836994546500236414, 17.95060345994707518, -5.000000000000000000 ) ) ;
#74009=CARTESIAN_POINT ( 'NONE',  ( 9.439578325719789831, 141.9252321839973092, 8.673617380357923939E-16 ) ) ;
#74035=CARTESIAN_POINT ( 'NONE',  ( 4.474623633717270010, 142.5192855048741762, 5.000000000000000888 ) ) ;
#74048=SURFACE_STYLE_FILL_AREA ( #25004 ) ;
#74076=DIRECTION ( 'NONE',  ( 0.000000000000000000, 0.000000000000000000, -1.000000000000000000 ) ) ;
#74155=ORIENTED_EDGE ( 'NONE', *, *, #47662, .T. ) ;
#74168=CARTESIAN_POINT ( 'NONE',  ( -5.899761283606826723, 4.638522211504596093, 5.000000000000000000 ) ) ;
#74266=AXIS2_PLACEMENT_3D ( 'NONE', #72511, #37540, #47166 ) ;
#74283=FILL_AREA_STYLE_COLOUR ( '', #69507 ) ;
#74296=CARTESIAN_POINT ( 'NONE',  ( 0.000000000000000000, 0.000000000000000000, 5.000000000000000000 ) ) ;
#74742=CARTESIAN_POINT ( 'NONE',  ( 2.955787000303736534, 53.34311400849869500, -5.000000000000000888 ) ) ;
#74794=VERTEX_POINT ( 'NONE', #79621 ) ;
#74807=CARTESIAN_POINT ( 'NONE',  ( -4.921335115252323256, 6.865562341691512138, 5.000000000000000000 ) ) ;
#74885=CIRCLE ( 'NONE', #42182, 5.000000000000000000 ) ;
#75099=CARTESIAN_POINT ( 'NONE',  ( -10.32854822922036853, 7.030784501320381352, -4.999999999999837463 ) ) ;
#75122=( GEOMETRIC_REPRESENTATION_CONTEXT ( 3 ) GLOBAL_UNCERTAINTY_ASSIGNED_CONTEXT ( ( #55527 ) ) GLOBAL_UNIT_ASSIGNED_CONTEXT ( ( #17837, #94919, #3773 ) ) REPRESENTATION_CONTEXT ( 'NONE', 'WORKASPACE' ) );
#75129=CARTESIAN_POINT ( 'NONE',  ( -5.956988534971662475, 4.556784786910193397, -5.000000000000000000 ) ) ;
#75261=EDGE_CURVE ( 'NONE', #65330, #18064, #65084, .T. ) ;
#75280=CARTESIAN_POINT ( 'NONE',  ( 2.849088492170978260, 70.33537520974232393, -4.999999999999997335 ) ) ;
#75361=( NAMED_UNIT ( * ) SI_UNIT ( $, .STERADIAN. ) SOLID_ANGLE_UNIT ( ) );
#75366=CARTESIAN_POINT ( 'NONE',  ( -0.000000000000000000, 0.000000000000000000, -5.000000000000000000 ) ) ;
#75431=CARTESIAN_POINT ( 'NONE',  ( -14.54015256618497176, 142.2617268803927573, -5.000000000000000000 ) ) ;
#75646=CARTESIAN_POINT ( 'NONE',  ( -5.888827218543791986, 4.654238857465189838, -4.999999999999999112 ) ) ;
#75680=FILL_AREA_STYLE_COLOUR ( '', #32504 ) ;
#75774=DIRECTION ( 'NONE',  ( -0.000000000000000000, -0.000000000000000000, 1.000000000000000000 ) ) ;
#75813=( LENGTH_UNIT ( ) NAMED_UNIT ( * ) SI_UNIT ( .MILLI., .METRE. ) );
#75822=CARTESIAN_POINT ( 'NONE',  ( 3.757222014067311378, 19.36722785790621870, -5.000000000000000888 ) ) ;
#75901=CARTESIAN_POINT ( 'NONE',  ( -3.819639294367488613, 133.7087141186266877, 4.999999999999997335 ) ) ;
#75938=TOROIDAL_SURFACE ( 'NONE', #46689, 7.500000000000006217, 5.000000000000000000 ) ;
#75947=EDGE_LOOP ( 'NONE', ( #17829, #97155, #82361, #55481 ) ) ;
#75983=AXIS2_PLACEMENT_3D ( 'NONE', #85024, #52111, #17644 ) ;
#75992=CARTESIAN_POINT ( 'NONE',  ( 0.000000000000000000, 152.0000000000000000, 0.000000000000000000 ) ) ;
#76002=CARTESIAN_POINT ( 'NONE',  ( 7.849089830965388259, 81.65314728018610424, 0.000000000000000000 ) ) ;
#76172=CARTESIAN_POINT ( 'NONE',  ( -6.339665615494448403, 4.010265277135025563, -5.000000000000000000 ) ) ;
#76190=( NAMED_UNIT ( * ) SI_UNIT ( $, .STERADIAN. ) SOLID_ANGLE_UNIT ( ) );
#76218=VERTEX_POINT ( 'NONE', #61497 ) ;
#76343=CARTESIAN_POINT ( 'NONE',  ( 3.225563553360571767, 36.35307765080715825, -4.999999999999999112 ) ) ;
#76367=DIRECTION ( 'NONE',  ( -0.000000000000000000, -1.000000000000000000, -0.000000000000000000 ) ) ;
#76424=CARTESIAN_POINT ( 'NONE',  ( -8.340586800786125465, 120.4027948985839913, 5.000000000000000000 ) ) ;
#76488=EDGE_CURVE ( 'NONE', #96258, #65330, #96294, .T. ) ;
#76502=DIRECTION ( 'NONE',  ( 0.000000000000000000, 0.000000000000000000, -1.000000000000000000 ) ) ;
#76529=CARTESIAN_POINT ( 'NONE',  ( 8.020869781912113083, 104.2554943876038180, 0.000000000000000000 ) ) ;
#76700=EDGE_CURVE ( 'NONE', #106589, #98095, #79027, .T. ) ;
#76705=FILL_AREA_STYLE ('',( #85897 ) ) ;
#76706=CARTESIAN_POINT ( 'NONE',  ( -10.11479301378070517, 7.336058586181116503, 0.000000000000000000 ) ) ;
#76730=CARTESIAN_POINT ( 'NONE',  ( -5.563220219054898941, 5.178627182129336148, -5.000000000000000000 ) ) ;
#76838=STYLED_ITEM ( 'NONE', ( #65966 ), #14500 ) ;
#76891=AXIS2_PLACEMENT_3D ( 'NONE', #7308, #32696, #72585 ) ;
#76927=EDGE_CURVE ( 'NONE', #31480, #83314, #79627, .T. ) ;
#76963=CARTESIAN_POINT ( 'NONE',  ( -9.061657590037185628, 137.7585088365954107, -1.734723475898753647E-15 ) ) ;
#77071=CARTESIAN_POINT ( 'NONE',  ( 8.441132293785154062, 123.9914807902427327, -1.229386795015411088E-12 ) ) ;
#77077=EDGE_LOOP ( 'NONE', ( #35682, #32406, #42933, #23490 ) ) ;
#77182=CARTESIAN_POINT ( 'NONE',  ( -9.206359606520587491, 139.5792630852731691, 0.000000000000000000 ) ) ;
#77251=PRESENTATION_STYLE_ASSIGNMENT (( #60554 ) ) ;
#77252=CARTESIAN_POINT ( 'NONE',  ( -9.943426265976000877, 7.591391547524681371, -5.000000000000000000 ) ) ;
#77280=CARTESIAN_POINT ( 'NONE',  ( 8.588409832247142717, 128.2015064896668264, -5.000000000000000000 ) ) ;
#77365=CARTESIAN_POINT ( 'NONE',  ( 4.474408960159419024, 9.482498132260746004, 5.000000000000000888 ) ) ;
#77509=CARTESIAN_POINT ( 'NONE',  ( -8.147102310908991285, 111.6559345260855594, 5.000000000000000888 ) ) ;
#77610=CARTESIAN_POINT ( 'NONE',  ( 7.955546711085368372, 53.39389859137057925, 5.000000000007370105 ) ) ;
#77717=CARTESIAN_POINT ( 'NONE',  ( -8.383456159752070036, 30.02471915937834623, -0.000000000000000000 ) ) ;
#77788=CARTESIAN_POINT ( 'NONE',  ( -9.832775748058654841, 7.875845744486726474, -5.000000000000000888 ) ) ;
#77813=CARTESIAN_POINT ( 'NONE',  ( -3.293703171889100112, 33.36073719191674058, -5.000000000000000000 ) ) ;
#77815=CARTESIAN_POINT ( 'NONE',  ( 9.517802786884892896, 142.5467050669339528, -5.000000000000310862 ) ) ;
#77871=ORIENTED_EDGE ( 'NONE', *, *, #98165, .F. ) ;
#77898=CARTESIAN_POINT ( 'NONE',  ( 4.322615621094100469, 10.89057051264452625, 4.999999999999999112 ) ) ;
#78033=CARTESIAN_POINT ( 'NONE',  ( -9.998846395930074848, 7.501654003239973889, 0.000000000000000000 ) ) ;
#78108=( GEOMETRIC_REPRESENTATION_CONTEXT ( 3 ) GLOBAL_UNCERTAINTY_ASSIGNED_CONTEXT ( ( #68614 ) ) GLOBAL_UNIT_ASSIGNED_CONTEXT ( ( #56210, #24450, #31989 ) ) REPRESENTATION_CONTEXT ( 'NONE', 'WORKASPACE' ) );
#78176=DIRECTION ( 'NONE',  ( 0.000000000000000000, 0.000000000000000000, -1.000000000000000000 ) ) ;
#78229=CARTESIAN_POINT ( 'NONE',  ( 7.849088363683611291, 76.00000000000000000, 5.000000000000000000 ) ) ;
#78277=CARTESIAN_POINT ( 'NONE',  ( 7.849088607700290154, 70.40480431129584815, 1.301042606982605321E-15 ) ) ;
#78303=CARTESIAN_POINT ( 'NONE',  ( -4.088019673764939910, 13.67890778943449526, -5.000000000000000888 ) ) ;
#78310=FILL_AREA_STYLE ('',( #37367 ) ) ;
#78330=CARTESIAN_POINT ( 'NONE',  ( 2.849089834143495814, 70.33461465726148276, -5.000000000000000000 ) ) ;
#78421=CARTESIAN_POINT ( 'NONE',  ( 5.000000000000000888, 6.123233995736767268E-16, 5.000000000000000000 ) ) ;
#78466=ORIENTED_EDGE ( 'NONE', *, *, #79912, .F. ) ;
#78555=CARTESIAN_POINT ( 'NONE',  ( -9.596328384832000680, 8.973060046492864927, 5.000000000000158984 ) ) ;
#78601=CARTESIAN_POINT ( 'NONE',  ( -7.009057377284643842, 5.325693897448008585, -4.838501632524188523 ) ) ;
#78720=FILL_AREA_STYLE ('',( #70651 ) ) ;
#78800=CARTESIAN_POINT ( 'NONE',  ( 8.731350795034574119, 131.9383239543996922, 0.000000000000000000 ) ) ;
#78828=CARTESIAN_POINT ( 'NONE',  ( -8.570032633477826067, 24.09669418278768660, -5.000000000001270095 ) ) ;
#78859=CARTESIAN_POINT ( 'NONE',  ( 3.443342638033509484, 124.1418742747060548, -5.000000000000000000 ) ) ;
#79012=UNCERTAINTY_MEASURE_WITH_UNIT (LENGTH_MEASURE( 1.000000000000000082E-05 ), #24814, 'distance_accuracy_value', 'NONE');
#79027=CIRCLE ( 'NONE', #15346, 7.500000000000000888 ) ;
#79090=CARTESIAN_POINT ( 'NONE',  ( -9.838569036983576765, 7.857203345569047315, 5.000000000000000888 ) ) ;
#79105=DIRECTION ( 'NONE',  ( -1.000000000000000000, 0.000000000000000000, 0.000000000000000000 ) ) ;
#79125=FACE_OUTER_BOUND ( 'NONE', #63631, .T. ) ;
#79173=ORIENTED_EDGE ( 'NONE', *, *, #86303, .T. ) ;
#79174=EDGE_LOOP ( 'NONE', ( #95234, #25442, #103349, #96821 ) ) ;
#79266=ORIENTED_EDGE ( 'NONE', *, *, #95429, .F. ) ;
#79345=FILL_AREA_STYLE ('',( #101642 ) ) ;
#79362=CARTESIAN_POINT ( 'NONE',  ( -8.066622878819057263, 44.48464632161675780, 0.000000000000000000 ) ) ;
#79391=TOROIDAL_SURFACE ( 'NONE', #138, 10.00000000000000000, 5.000000000000000000 ) ;
#79394=CARTESIAN_POINT ( 'NONE',  ( 8.224453817191152538, 115.5406540063856085, -5.000000000001228351 ) ) ;
#79455=CARTESIAN_POINT ( 'NONE',  ( 4.561000490385944239, 8.778822500554452901, 5.000000000000000000 ) ) ;
#79601=DIRECTION ( 'NONE',  ( -0.1659550938519105956, -0.9861333108787085910, 0.000000000000000000 ) ) ;
#79612=CARTESIAN_POINT ( 'NONE',  ( -9.550648135838782693, 9.268430070245118557, 0.000000000000000000 ) ) ;
#79621=CARTESIAN_POINT ( 'NONE',  ( -4.678819457397884740, 143.9212778189118467, 5.000000000000000000 ) ) ;
#79627=B_SPLINE_CURVE_WITH_KNOTS ( 'NONE', 3,
 ( #21156, #38899, #30284, #5458, #86404, #62644, #22731, #38380, #79861, #103100, #88506, #12996, #96065, #105213, #45921, #37332, #78277, #4393, #6497, #96599, #12466, #45399, #22197, #55048, #87977, #72307, #78800, #54506, #21673, #14058, #70724, #71762, #4933, #30826 ),
 .UNSPECIFIED., .F., .F.,
 ( 4, 2, 2, 2, 2, 2, 2, 2, 2, 2, 2, 2, 2, 2, 2, 2, 4 ),
 ( 0.000000000000000000, 0.002098190355514029017, 0.004196380711028058035, 0.008392761422056110865, 0.01678552284411221826, 0.02517828426616832566, 0.03357104568822444346, 0.05035656853233669988, 0.06714209137644897019, 0.08392761422056123355, 0.1007131370646734969, 0.1091058984867296217, 0.1174986599087857603, 0.1258914213308418850, 0.1300878020418699821, 0.1321859923973840445, 0.1342841827528981069 ),
 .UNSPECIFIED. ) ;
#79661=CARTESIAN_POINT ( 'NONE',  ( 3.225573779814643771, 115.6473726989443520, -5.000000000000000000 ) ) ;
#79708=ADVANCED_FACE ( 'NONE', ( #71148 ), #79391, .T. ) ;
#79729=CARTESIAN_POINT ( 'NONE',  ( -3.742273759344161732, 132.3176420647150451, 5.000000000000000000 ) ) ;
#79790=ORIENTED_EDGE ( 'NONE', *, *, #95077, .T. ) ;
#79861=CARTESIAN_POINT ( 'NONE',  ( 8.619464431494504808, 22.85699679202996393, -9.629649721936179265E-31 ) ) ;
#79886=CARTESIAN_POINT ( 'NONE',  ( -3.003085654062773280, 102.9757869438805642, -5.000000000000000000 ) ) ;
#79911=DIRECTION ( 'NONE',  ( -0.000000000000000000, -0.000000000000000000, 1.000000000000000000 ) ) ;
#79912=EDGE_CURVE ( 'NONE', #61174, #10145, #31240, .T. ) ;
#79918=CARTESIAN_POINT ( 'NONE',  ( 9.609486011791085858, 8.908497650349774588, 0.000000000000000000 ) ) ;
#79976=CARTESIAN_POINT ( 'NONE',  ( 8.642223818571391547, 22.39656424817261993, 0.000000000000000000 ) ) ;
#80001=PRESENTATION_STYLE_ASSIGNMENT (( #81572 ) ) ;
#80030=DIRECTION ( 'NONE',  ( 1.000000000000000000, 0.000000000000000000, 0.000000000000000000 ) ) ;
#80141=CARTESIAN_POINT ( 'NONE',  ( -9.946294137122949408, 7.586021176442817371, 0.000000000000000000 ) ) ;
#80189=FACE_BOUND ( 'NONE', #31448, .T. ) ;
#80245=CARTESIAN_POINT ( 'NONE',  ( -3.548074437533462078, 24.62734600915379701, 4.999999999999998224 ) ) ;
#80266=AXIS2_PLACEMENT_3D ( 'NONE', #18753, #59185, #92063 ) ;
#80349=DIRECTION ( 'NONE',  ( -0.9861333108788029600, -0.1659550938513498497, 8.881784197001250351E-16 ) ) ;
#80410=CARTESIAN_POINT ( 'NONE',  ( -8.002730990579065562, 102.9130261956584746, -4.999999999992380317 ) ) ;
#80425=UNCERTAINTY_MEASURE_WITH_UNIT (LENGTH_MEASURE( 1.000000000000000082E-05 ), #32744, 'distance_accuracy_value', 'NONE');
#80430=VECTOR ( 'NONE', #59377, 1000.000000000000000 ) ;
#80501=CARTESIAN_POINT ( 'NONE',  ( 9.517802786874057119, 9.453294933053111748, 5.000000000000309086 ) ) ;
#80528=SURFACE_STYLE_FILL_AREA ( #47099 ) ;
#80759=VERTEX_POINT ( 'NONE', #103342 ) ;
#80823=FILL_AREA_STYLE ('',( #21565 ) ) ;
#80948=CARTESIAN_POINT ( 'NONE',  ( -8.734619362698921918, 132.0311980842794526, -2.602085213900631332E-15 ) ) ;
#80973=CARTESIAN_POINT ( 'NONE',  ( 4.259258436597560760, 11.59113387677236595, -5.000000000000000000 ) ) ;
#81033=CARTESIAN_POINT ( 'NONE',  ( 8.763392006745778673, 19.59990099439108135, 0.000000000000000000 ) ) ;
#81130=EDGE_CURVE ( 'NONE', #10915, #84815, #63945, .T. ) ;
#81318=CARTESIAN_POINT ( 'NONE',  ( -4.678819457397875858, 143.9212778189118183, 5.000000000000004441 ) ) ;
#81547=CARTESIAN_POINT ( 'NONE',  ( 8.588409832245909925, 23.79849351031133509, 4.999999999998157918 ) ) ;
#81572=SURFACE_STYLE_USAGE ( .BOTH. , #97773 ) ;
#81573=CARTESIAN_POINT ( 'NONE',  ( 2.849088235197430485, 70.33548021428394748, 5.000000000000000000 ) ) ;
#81581=COLOUR_RGB ( '', 0.66274510, 0.83137255, 0.94901961) ;
#81635=ORIENTED_EDGE ( 'NONE', *, *, #22212, .T. ) ;
#81713=CARTESIAN_POINT ( 'NONE',  ( -9.999733828770100530, 7.500380388541294074, 0.000000000000000000 ) ) ;
#81724=CARTESIAN_POINT ( 'NONE',  ( -9.590257352332137941, 7.202916011546355080, 2.216224026219065557 ) ) ;
#81791=EDGE_CURVE ( 'NONE', #55300, #98139, #57047, .T. ) ;
#81942=FACE_OUTER_BOUND ( 'NONE', #101094, .T. ) ;
#82001=CARTESIAN_POINT ( 'NONE',  ( -9.609486011791425142, 143.0915023496523020, -5.000000000000000888 ) ) ;
#82034=CARTESIAN_POINT ( 'NONE',  ( 7.869432500659452323, 64.69453614009762532, -5.000000000000000888 ) ) ;
#82052=EDGE_CURVE ( 'NONE', #98139, #55300, #60552, .T. ) ;
#82097=CARTESIAN_POINT ( 'NONE',  ( 4.259258436598990727, 140.4088661232431150, 5.000000000000000000 ) ) ;
#82103=ORIENTED_EDGE ( 'NONE', *, *, #81130, .T. ) ;
#82119=FILL_AREA_STYLE_COLOUR ( '', #52305 ) ;
#82173=SURFACE_SIDE_STYLE ('',( #90818 ) ) ;
#82201=EDGE_CURVE ( 'NONE', #52915, #83314, #105342, .T. ) ;
#82263=CARTESIAN_POINT ( 'NONE',  ( -5.904546178069103313, 4.631679053609773611, 5.000000000000000000 ) ) ;
#82314=CARTESIAN_POINT ( 'NONE',  ( 3.641358249959525395, 22.19731953646417466, -4.999999999999999112 ) ) ;
#82334=PRODUCT_DEFINITION_CONTEXT ( 'detailed design', #87919, 'design' ) ;
#82361=ORIENTED_EDGE ( 'NONE', *, *, #57418, .T. ) ;
#82412=AXIS2_PLACEMENT_3D ( 'NONE', #22962, #54753, #72540 ) ;
#82646=CARTESIAN_POINT ( 'NONE',  ( 3.363293968491885888, 121.3118620733033168, 5.000000000000000000 ) ) ;
#82711=CARTESIAN_POINT ( 'NONE',  ( -4.261688254080127969, 11.55297089381481790, -5.000000000000000888 ) ) ;
#82818=CARTESIAN_POINT ( 'NONE',  ( -9.896718155645521264, 7.425134178940658636, 1.133880678298145650 ) ) ;
#82917=SURFACE_STYLE_FILL_AREA ( #31733 ) ;
#82920=DIRECTION ( 'NONE',  ( -0.9861333108788020718, 0.1659550938513554286, 0.000000000000000000 ) ) ;
#82961=( BOUNDED_SURFACE ( )  B_SPLINE_SURFACE ( 3, 2, ( 
 ( #43288, #43814, #67042 ),
 ( #10373, #51899, #76172 ),
 ( #50824, #75099, #19055 ),
 ( #19595, #51366, #2274 ),
 ( #76706, #35225, #27146 ),
 ( #84810, #33621, #84278 ),
 ( #1196, #66493, #99375 ),
 ( #17965, #34164, #27684 ),
 ( #11429, #99920, #92353 ),
 ( #26094, #92894, #91841 ),
 ( #10894, #1746, #44356 ),
 ( #35773, #83729, #68648 ),
 ( #101528, #9840, #52427 ),
 ( #60556, #58411, #91323 ),
 ( #85343, #68092, #75646 ),
 ( #67575, #34701, #18504 ),
 ( #9306, #59488, #50304 ),
 ( #100987, #100456, #60033 ),
 ( #26615, #77252, #21699 ),
 ( #53508, #54533, #29274 ),
 ( #4421, #77788, #87477 ),
 ( #61080, #38404, #14082 ),
 ( #45428, #95047, #36310 ),
 ( #62154, #96090, #36829 ),
 ( #63199, #104167, #71271 ),
 ( #54011, #30309, #69177 ),
 ( #12494, #52975, #4959 ),
 ( #21181, #22226, #85898 ),
 ( #69699, #37358, #46989 ),
 ( #46475, #103644, #78303 ),
 ( #37890, #86955, #70222 ),
 ( #28739, #102044, #20123 ),
 ( #13021, #103123, #93972 ),
 ( #45948, #78828, #70748 ),
 ( #3366, #29793, #102590 ),
 ( #5484, #11972, #55073 ),
 ( #62671, #95560, #13557 ),
 ( #79362, #88001, #44901 ),
 ( #20668, #3896, #28211 ),
 ( #61624, #94517, #86434 ),
 ( #47521, #5999, #38922 ),
 ( #90109, #97653, #106273 ),
 ( #71790, #73374, #16753 ),
 ( #7057, #98196, #105240 ),
 ( #41032, #80410, #79886 ),
 ( #40499, #65310, #39976 ),
 ( #48041, #96619, #89058 ),
 ( #31384, #104701, #15155 ),
 ( #97133, #6523, #49101 ),
 ( #57723, #105756, #24866 ),
 ( #80948, #64262, #24350 ),
 ( #32436, #22757, #57194 ),
 ( #39458, #73913, #23280 ),
 ( #48573, #16214, #30852 ),
 ( #56118, #98713, #89589 ),
 ( #7577, #72844, #31898 ),
 ( #72336, #55593, #64778 ),
 ( #23825, #82001, #88530 ) ),
 .UNSPECIFIED., .F., .F., .F. ) 
 B_SPLINE_SURFACE_WITH_KNOTS ( ( 4, 2, 2, 2, 2, 2, 2, 2, 2, 2, 2, 2, 2, 2, 2, 2, 2, 2, 2, 2, 2, 2, 2, 2, 2, 2, 2, 2, 4 ),
 ( 3, 3 ),
 ( 0.05905452279715409786, 0.05961352906526162787, 0.05989303219931539635, 0.05996290798282884194, 0.05999784587458556473, 0.06000658034752474196, 0.06001531482046391919, 0.06003278376634228058, 0.06017253533336916482, 0.06129054786958423873, 0.06240856040579931263, 0.06352657294201438654, 0.06464458547822946044, 0.06576259801444453434, 0.06799862308687466828, 0.07247067323173495001, 0.07694272337659524563, 0.08588682366631580911, 0.09483092395603638647, 0.1127191245354775273, 0.1306073251149186820, 0.1484955256943598367, 0.1663837262738009914, 0.1753278265635215549, 0.1842719268532421184, 0.1932160271429627096, 0.1976880772878230053, 0.1999241023602531531, 0.2021601274326832731 ),
 ( 0.000000000000000000, 1.000000000000000000 ),
 .UNSPECIFIED. ) 
 GEOMETRIC_REPRESENTATION_ITEM ( )  RATIONAL_B_SPLINE_SURFACE ( (
 ( 1.000000000000000000, 0.7071067811865475727, 1.000000000000000000),
 ( 1.000000000000000000, 0.7071067811865475727, 1.000000000000000000),
 ( 1.000000000000000000, 0.7071067811865475727, 1.000000000000000000),
 ( 1.000000000000000000, 0.7071067811865475727, 1.000000000000000000),
 ( 1.000000000000000000, 0.7071067811865475727, 1.000000000000000000),
 ( 1.000000000000000000, 0.7071067811865475727, 1.000000000000000000),
 ( 1.000000000000000000, 0.7071067811865475727, 1.000000000000000000),
 ( 1.000000000000000000, 0.7071067811865475727, 1.000000000000000000),
 ( 1.000000000000000000, 0.7071067811865475727, 1.000000000000000000),
 ( 1.000000000000000000, 0.7071067811865475727, 1.000000000000000000),
 ( 1.000000000000000000, 0.7071067811865475727, 1.000000000000000000),
 ( 1.000000000000000000, 0.7071067811865475727, 1.000000000000000000),
 ( 1.000000000000000000, 0.7071067811865475727, 1.000000000000000000),
 ( 1.000000000000000000, 0.7071067811865475727, 1.000000000000000000),
 ( 1.000000000000000000, 0.7071067811865475727, 1.000000000000000000),
 ( 1.000000000000000000, 0.7071067811865475727, 1.000000000000000000),
 ( 1.000000000000000000, 0.7071067811865475727, 1.000000000000000000),
 ( 1.000000000000000000, 0.7071067811865475727, 1.000000000000000000),
 ( 1.000000000000000000, 0.7071067811865474617, 1.000000000000000000),
 ( 1.000000000000000000, 0.7071067811865474617, 1.000000000000000000),
 ( 1.000000000000000000, 0.7071067811865475727, 1.000000000000000000),
 ( 1.000000000000000000, 0.7071067811865475727, 1.000000000000000000),
 ( 1.000000000000000000, 0.7071067811865475727, 1.000000000000000000),
 ( 1.000000000000000000, 0.7071067811865475727, 1.000000000000000000),
 ( 1.000000000000000000, 0.7071067811865475727, 1.000000000000000000),
 ( 1.000000000000000000, 0.7071067811865475727, 1.000000000000000000),
 ( 1.000000000000000000, 0.7071067811865474617, 1.000000000000000000),
 ( 1.000000000000000000, 0.7071067811865474617, 1.000000000000000000),
 ( 1.000000000000000000, 0.7071067811865475727, 1.000000000000000000),
 ( 1.000000000000000000, 0.7071067811865475727, 1.000000000000000000),
 ( 1.000000000000000000, 0.7071067811865475727, 1.000000000000000000),
 ( 1.000000000000000000, 0.7071067811865475727, 1.000000000000000000),
 ( 1.000000000000000000, 0.7071067811865475727, 1.000000000000000000),
 ( 1.000000000000000000, 0.7071067811865475727, 1.000000000000000000),
 ( 1.000000000000000000, 0.7071067811865474617, 1.000000000000000000),
 ( 1.000000000000000000, 0.7071067811865474617, 1.000000000000000000),
 ( 1.000000000000000000, 0.7071067811865475727, 1.000000000000000000),
 ( 1.000000000000000000, 0.7071067811865475727, 1.000000000000000000),
 ( 1.000000000000000000, 0.7071067811865474617, 1.000000000000000000),
 ( 1.000000000000000000, 0.7071067811865474617, 1.000000000000000000),
 ( 1.000000000000000000, 0.7071067811865475727, 1.000000000000000000),
 ( 1.000000000000000000, 0.7071067811865475727, 1.000000000000000000),
 ( 1.000000000000000000, 0.7071067811865474617, 1.000000000000000000),
 ( 1.000000000000000000, 0.7071067811865474617, 1.000000000000000000),
 ( 1.000000000000000000, 0.7071067811865475727, 1.000000000000000000),
 ( 1.000000000000000000, 0.7071067811865475727, 1.000000000000000000),
 ( 1.000000000000000000, 0.7071067811865475727, 1.000000000000000000),
 ( 1.000000000000000000, 0.7071067811865475727, 1.000000000000000000),
 ( 1.000000000000000000, 0.7071067811865475727, 1.000000000000000000),
 ( 1.000000000000000000, 0.7071067811865475727, 1.000000000000000000),
 ( 1.000000000000000000, 0.7071067811865473507, 1.000000000000000000),
 ( 1.000000000000000000, 0.7071067811865473507, 1.000000000000000000),
 ( 1.000000000000000000, 0.7071067811865475727, 1.000000000000000000),
 ( 1.000000000000000000, 0.7071067811865475727, 1.000000000000000000),
 ( 1.000000000000000000, 0.7071067811865475727, 1.000000000000000000),
 ( 1.000000000000000000, 0.7071067811865475727, 1.000000000000000000),
 ( 1.000000000000000000, 0.7071067811865475727, 1.000000000000000000),
 ( 1.000000000000000000, 0.7071067811865475727, 1.000000000000000000) ) ) 
 REPRESENTATION_ITEM ( '' )  SURFACE ( )  );
#83155=SURFACE_SIDE_STYLE ('',( #50254 ) ) ;
#83194=TOROIDAL_SURFACE ( 'NONE', #50454, 7.500000000000006217, 5.000000000000000000 ) ;
#83267=MECHANICAL_DESIGN_GEOMETRIC_PRESENTATION_REPRESENTATION('',(#2341),#105658);
#83314=VERTEX_POINT ( 'NONE', #34950 ) ;
#83345=CARTESIAN_POINT ( 'NONE',  ( -9.999999999999982236, 7.499999999999973355, 0.000000000000000000 ) ) ;
#83457=SURFACE_STYLE_USAGE ( .BOTH. , #50542 ) ;
#83509=CARTESIAN_POINT ( 'NONE',  ( 0.000000000000000000, 152.0000000000000000, -5.000000000000000000 ) ) ;
#83609=VERTEX_POINT ( 'NONE', #13811 ) ;
#83693=DIRECTION ( 'NONE',  ( 0.000000000000000000, 0.000000000000000000, -1.000000000000000000 ) ) ;
#83729=CARTESIAN_POINT ( 'NONE',  ( -9.999497344918166775, 7.500719060599902122, -5.000000000000000888 ) ) ;
#83748=DIRECTION ( 'NONE',  ( 0.000000000000000000, 0.000000000000000000, -1.000000000000000000 ) ) ;
#83841=ORIENTED_EDGE ( 'NONE', *, *, #58259, .T. ) ;
#83912=CARTESIAN_POINT ( 'NONE',  ( 2.869469304594349790, 64.67108097164965841, -5.000000000000001776 ) ) ;
#83978=DIRECTION ( 'NONE',  ( -1.000000000000000000, 0.000000000000000000, 0.000000000000000000 ) ) ;
#83997=CARTESIAN_POINT ( 'NONE',  ( -8.568812041302383165, 127.6722392238321078, 4.999999999999365841 ) ) ;
#84072=( LENGTH_UNIT ( ) NAMED_UNIT ( * ) SI_UNIT ( .MILLI., .METRE. ) );
#84155=AXIS2_PLACEMENT_3D ( 'NONE', #12509, #70763, #22239 ) ;
#84161=DIRECTION ( 'NONE',  ( 0.000000000000000000, 0.000000000000000000, -1.000000000000000000 ) ) ;
#84277=DIRECTION ( 'NONE',  ( 0.000000000000000000, 0.000000000000000000, -1.000000000000000000 ) ) ;
#84278=CARTESIAN_POINT ( 'NONE',  ( -5.952234287511010358, 4.563574555944671651, -5.000000000000000000 ) ) ;
#84359=ORIENTED_EDGE ( 'NONE', *, *, #30428, .T. ) ;
#84540=CARTESIAN_POINT ( 'NONE',  ( -8.971954110056353571, 136.3305255231049671, -1.734723475998474934E-15 ) ) ;
#84639=CARTESIAN_POINT ( 'NONE',  ( 2.955796066023812063, 53.34212538443676976, 5.000000000000000000 ) ) ;
#84810=CARTESIAN_POINT ( 'NONE',  ( -10.04799450895599122, 7.431456737699883242, 0.000000000000000000 ) ) ;
#84815=VERTEX_POINT ( 'NONE', #43055 ) ;
#84828=AXIS2_PLACEMENT_3D ( 'NONE', #94735, #4648, #28971 ) ;
#84892=( GEOMETRIC_REPRESENTATION_CONTEXT ( 3 ) GLOBAL_UNCERTAINTY_ASSIGNED_CONTEXT ( ( #2785 ) ) GLOBAL_UNIT_ASSIGNED_CONTEXT ( ( #98574, #7429, #75361 ) ) REPRESENTATION_CONTEXT ( 'NONE', 'WORKASPACE' ) );
#84934=CIRCLE ( 'NONE', #52191, 5.000000000000000888 ) ;
#84977=SURFACE_SIDE_STYLE ('',( #59646 ) ) ;
#84981=ORIENTED_EDGE ( 'NONE', *, *, #95077, .F. ) ;
#85004=ADVANCED_FACE ( 'NONE', ( #79125 ), #5849, .T. ) ;
#85024=CARTESIAN_POINT ( 'NONE',  ( 4.678819457397440651, 8.078722181090837395, 0.000000000000000000 ) ) ;
#85067=CARTESIAN_POINT ( 'NONE',  ( -8.568812041277357849, 127.6722392238329462, 0.000000000000000000 ) ) ;
#85145=ORIENTED_EDGE ( 'NONE', *, *, #131, .T. ) ;
#85164=( GEOMETRIC_REPRESENTATION_CONTEXT ( 3 ) GLOBAL_UNCERTAINTY_ASSIGNED_CONTEXT ( ( #42270 ) ) GLOBAL_UNIT_ASSIGNED_CONTEXT ( ( #5767, #6824, #21984 ) ) REPRESENTATION_CONTEXT ( 'NONE', 'WORKASPACE' ) );
#85167=CARTESIAN_POINT ( 'NONE',  ( 7.849086896557445847, 70.34805173277894141, 0.000000000000000000 ) ) ;
#85219=DIRECTION ( 'NONE',  ( -1.000000000000000000, 0.000000000000000000, 0.000000000000000000 ) ) ;
#85229=CARTESIAN_POINT ( 'NONE',  ( 5.000000000000002665, 152.0000000000000000, 5.000000000000000000 ) ) ;
#85242=( LENGTH_UNIT ( ) NAMED_UNIT ( * ) SI_UNIT ( .MILLI., .METRE. ) );
#85279=CARTESIAN_POINT ( 'NONE',  ( 5.000000000000002665, 152.0000000000000000, -5.000000000000000000 ) ) ;
#85342=FACE_OUTER_BOUND ( 'NONE', #20519, .T. ) ;
#85343=CARTESIAN_POINT ( 'NONE',  ( -9.998567040938999284, 7.502056690389962590, 0.000000000000000000 ) ) ;
#85372=MECHANICAL_DESIGN_GEOMETRIC_PRESENTATION_REPRESENTATION('',(#30275),#24282);
#85374=CARTESIAN_POINT ( 'NONE',  ( 7.849086896557461834, 81.65194826718307297, 2.456708681988599773E-12 ) ) ;
#85379=( NAMED_UNIT ( * ) PLANE_ANGLE_UNIT ( ) SI_UNIT ( $, .RADIAN. ) );
#85611=CARTESIAN_POINT ( 'NONE',  ( -8.420453562213536358, 123.3148673108814819, 0.000000000000000000 ) ) ;
#85717=CARTESIAN_POINT ( 'NONE',  ( 3.996301576410518308, 136.8773085153401894, 5.000000000000000888 ) ) ;
#85793=ORIENTED_EDGE ( 'NONE', *, *, #35676, .F. ) ;
#85826=CARTESIAN_POINT ( 'NONE',  ( -7.873155740944470793, 63.95458188447780401, 0.000000000000000000 ) ) ;
#85897=FILL_AREA_STYLE_COLOUR ( '', #73668 ) ;
#85898=CARTESIAN_POINT ( 'NONE',  ( -4.334700171289733284, 10.76211272510062678, -5.000000000000000888 ) ) ;
#85925=CARTESIAN_POINT ( 'NONE',  ( -4.678819457397884740, 143.9212778189118467, -5.000000000000000000 ) ) ;
#85926=CARTESIAN_POINT ( 'NONE',  ( 8.020865862485518250, 104.2551619145343835, -5.000000000000000888 ) ) ;
#85927=AXIS2_PLACEMENT_3D ( 'NONE', #16119, #90549, #16658 ) ;
#85928=CARTESIAN_POINT ( 'NONE',  ( -4.678819457397884740, 143.9212778189118467, -5.000000000000000000 ) ) ;
#85939=MECHANICAL_DESIGN_GEOMETRIC_PRESENTATION_REPRESENTATION('',(#61852),#70459);
#85987=AXIS2_PLACEMENT_3D ( 'NONE', #43972, #52048, #27303 ) ;
#86014=CARTESIAN_POINT ( 'NONE',  ( 3.443305032968360102, 27.85938107923988483, 4.999999999999997335 ) ) ;
#86153=CARTESIAN_POINT ( 'NONE',  ( -2.989987493987218414, 50.23304204759762825, 5.000000000000000000 ) ) ;
#86206=CARTESIAN_POINT ( 'NONE',  ( -7.984026910922526810, 6.036057507192810867, -4.337419204752972490 ) ) ;
#86224=EDGE_LOOP ( 'NONE', ( #89154, #42232 ) ) ;
#86243=TOROIDAL_SURFACE ( 'NONE', #105151, 7.500000000000006217, 5.000000000000000000 ) ;
#86303=EDGE_CURVE ( 'NONE', #98095, #70327, #73206, .T. ) ;
#86328=( NAMED_UNIT ( * ) SI_UNIT ( $, .STERADIAN. ) SOLID_ANGLE_UNIT ( ) );
#86362=CARTESIAN_POINT ( 'NONE',  ( -9.266991278717167546, 140.2840666555874805, -0.000000000000000000 ) ) ;
#86404=CARTESIAN_POINT ( 'NONE',  ( 9.209599246271393369, 12.38267295484908459, 0.000000000000000000 ) ) ;
#86434=CARTESIAN_POINT ( 'NONE',  ( -2.883699206286927996, 61.97772922454487343, -4.999999999999999112 ) ) ;
#86442=SURFACE_STYLE_USAGE ( .BOTH. , #88010 ) ;
#86448=CARTESIAN_POINT ( 'NONE',  ( 6.231493956936416723, 147.8264543773111654, 5.000000000000000000 ) ) ;
#86464=CARTESIAN_POINT ( 'NONE',  ( 3.021271035810708661, 104.3218411490978070, -5.000000000000000000 ) ) ;
#86539=ORIENTED_EDGE ( 'NONE', *, *, #105938, .F. ) ;
#86627=( BOUNDED_SURFACE ( )  B_SPLINE_SURFACE ( 3, 2, ( 
 ( #41406, #89962, #81318 ),
 ( #106124, #57570, #23662 ),
 ( #57044, #48949, #7966 ),
 ( #90494, #16603, #49494 ),
 ( #8503, #12222, #102306 ),
 ( #76963, #11685, #44078 ),
 ( #84540, #52681, #68357 ),
 ( #10625, #3079, #75901 ),
 ( #36025, #10103, #101255 ),
 ( #53233, #27409, #68899 ),
 ( #85067, #83997, #1999 ),
 ( #85611, #51621, #101773 ),
 ( #44620, #76424, #69424 ),
 ( #34947, #100174, #27939 ),
 ( #11149, #77509, #67818 ),
 ( #26343, #60802, #94225 ),
 ( #52152, #43014, #93694 ),
 ( #93157, #43544, #60286 ),
 ( #100700, #61335, #19324 ),
 ( #26867, #19846, #3622 ),
 ( #35482, #36555, #18773 ),
 ( #28456, #20390, #86153 ),
 ( #18222, #45152, #1462 ),
 ( #59737, #34424, #2539 ),
 ( #92614, #67296, #59204 ),
 ( #92081, #51076, #38143 ),
 ( #13276, #37081, #96356 ),
 ( #54797, #30565, #87200 ),
 ( #104418, #103888, #30034 ),
 ( #63994, #63463, #104967 ),
 ( #86681, #22486, #55327 ),
 ( #4152, #45675, #69946 ),
 ( #87730, #13809, #88254 ),
 ( #96870, #102844, #46721 ),
 ( #29011, #21947, #12752 ),
 ( #79612, #62924, #46204 ),
 ( #23004, #78555, #31108 ),
 ( #61877, #4685, #95818 ),
 ( #21417, #5213, #14333 ),
 ( #47240, #79090, #72059 ),
 ( #62394, #5727, #6242 ),
 ( #80141, #38651, #37618 ),
 ( #70481, #39179, #71517 ),
 ( #54257, #103376, #94771 ),
 ( #55840, #88779, #14869 ),
 ( #78033, #20919, #53753 ),
 ( #95288, #29523, #70997 ),
 ( #25125, #33747, #74168 ),
 ( #81713, #56378, #248 ),
 ( #89839, #33212, #82263 ),
 ( #105998, #105484, #40744 ),
 ( #58541, #65023, #90906 ),
 ( #106535, #31622, #73632 ),
 ( #8375, #23537, #32691 ),
 ( #41805, #6787, #16476 ),
 ( #90362, #17020, #24070 ),
 ( #7836, #24595, #56914 ),
 ( #15407, #65558, #49356 ),
 ( #98447, #15942, #99503 ),
 ( #41277, #48818, #57442 ) ),
 .UNSPECIFIED., .F., .F., .F. ) 
 B_SPLINE_SURFACE_WITH_KNOTS ( ( 4, 2, 2, 2, 2, 2, 2, 2, 2, 2, 2, 2, 2, 2, 2, 2, 2, 2, 2, 2, 2, 2, 2, 2, 2, 2, 2, 2, 2, 4 ),
 ( 3, 3 ),
 ( 0.06375477930561219975, 0.06599154682095068059, 0.06822831433628917530, 0.07270184936696613698, 0.07717538439764309866, 0.08164891942832006033, 0.09059598948967399756, 0.09954305955102793479, 0.1174371996737358093, 0.1353313397964436837, 0.1532254799191515582, 0.1711196200418594326, 0.1800666901032133560, 0.1890137601645672794, 0.1934872951952442410, 0.1979608302259212027, 0.2001975977412596974, 0.2013159814989289309, 0.2024343652565981921, 0.2035527490142674256, 0.2046711327719366591, 0.2057895165296059203, 0.2059293144993145641, 0.2059467892455281446, 0.2059555266186349209, 0.2059642639917417251, 0.2059992134841688860, 0.2060691124690232356, 0.2063487084084405510, 0.2069079002872751538 ),
 ( 0.000000000000000000, 1.000000000000000000 ),
 .UNSPECIFIED. ) 
 GEOMETRIC_REPRESENTATION_ITEM ( )  RATIONAL_B_SPLINE_SURFACE ( (
 ( 1.000000000000000000, 0.7071067811865474617, 1.000000000000000000),
 ( 1.000000000000000000, 0.7071067811865474617, 1.000000000000000000),
 ( 1.000000000000000000, 0.7071067811865474617, 1.000000000000000000),
 ( 1.000000000000000000, 0.7071067811865474617, 1.000000000000000000),
 ( 1.000000000000000000, 0.7071067811865476838, 1.000000000000000000),
 ( 1.000000000000000000, 0.7071067811865476838, 1.000000000000000000),
 ( 1.000000000000000000, 0.7071067811865476838, 1.000000000000000000),
 ( 1.000000000000000000, 0.7071067811865476838, 1.000000000000000000),
 ( 1.000000000000000000, 0.7071067811865474617, 1.000000000000000000),
 ( 1.000000000000000000, 0.7071067811865474617, 1.000000000000000000),
 ( 1.000000000000000000, 0.7071067811865475727, 1.000000000000000000),
 ( 1.000000000000000000, 0.7071067811865475727, 1.000000000000000000),
 ( 1.000000000000000000, 0.7071067811865474617, 1.000000000000000000),
 ( 1.000000000000000000, 0.7071067811865474617, 1.000000000000000000),
 ( 1.000000000000000000, 0.7071067811865475727, 1.000000000000000000),
 ( 1.000000000000000000, 0.7071067811865475727, 1.000000000000000000),
 ( 1.000000000000000000, 0.7071067811865475727, 1.000000000000000000),
 ( 1.000000000000000000, 0.7071067811865475727, 1.000000000000000000),
 ( 1.000000000000000000, 0.7071067811865474617, 1.000000000000000000),
 ( 1.000000000000000000, 0.7071067811865474617, 1.000000000000000000),
 ( 1.000000000000000000, 0.7071067811865475727, 1.000000000000000000),
 ( 1.000000000000000000, 0.7071067811865475727, 1.000000000000000000),
 ( 1.000000000000000000, 0.7071067811865475727, 1.000000000000000000),
 ( 1.000000000000000000, 0.7071067811865475727, 1.000000000000000000),
 ( 1.000000000000000000, 0.7071067811865475727, 1.000000000000000000),
 ( 1.000000000000000000, 0.7071067811865475727, 1.000000000000000000),
 ( 1.000000000000000000, 0.7071067811865475727, 1.000000000000000000),
 ( 1.000000000000000000, 0.7071067811865475727, 1.000000000000000000),
 ( 1.000000000000000000, 0.7071067811865475727, 1.000000000000000000),
 ( 1.000000000000000000, 0.7071067811865475727, 1.000000000000000000),
 ( 1.000000000000000000, 0.7071067811865475727, 1.000000000000000000),
 ( 1.000000000000000000, 0.7071067811865475727, 1.000000000000000000),
 ( 1.000000000000000000, 0.7071067811865475727, 1.000000000000000000),
 ( 1.000000000000000000, 0.7071067811865475727, 1.000000000000000000),
 ( 1.000000000000000000, 0.7071067811865475727, 1.000000000000000000),
 ( 1.000000000000000000, 0.7071067811865475727, 1.000000000000000000),
 ( 1.000000000000000000, 0.7071067811865475727, 1.000000000000000000),
 ( 1.000000000000000000, 0.7071067811865475727, 1.000000000000000000),
 ( 1.000000000000000000, 0.7071067811865475727, 1.000000000000000000),
 ( 1.000000000000000000, 0.7071067811865475727, 1.000000000000000000),
 ( 1.000000000000000000, 0.7071067811865475727, 1.000000000000000000),
 ( 1.000000000000000000, 0.7071067811865475727, 1.000000000000000000),
 ( 1.000000000000000000, 0.7071067811865475727, 1.000000000000000000),
 ( 1.000000000000000000, 0.7071067811865475727, 1.000000000000000000),
 ( 1.000000000000000000, 0.7071067811865475727, 1.000000000000000000),
 ( 1.000000000000000000, 0.7071067811865475727, 1.000000000000000000),
 ( 1.000000000000000000, 0.7071067811865475727, 1.000000000000000000),
 ( 1.000000000000000000, 0.7071067811865475727, 1.000000000000000000),
 ( 1.000000000000000000, 0.7071067811865475727, 1.000000000000000000),
 ( 1.000000000000000000, 0.7071067811865475727, 1.000000000000000000),
 ( 1.000000000000000000, 0.7071067811865475727, 1.000000000000000000),
 ( 1.000000000000000000, 0.7071067811865475727, 1.000000000000000000),
 ( 1.000000000000000000, 0.7071067811865475727, 1.000000000000000000),
 ( 1.000000000000000000, 0.7071067811865475727, 1.000000000000000000),
 ( 1.000000000000000000, 0.7071067811865475727, 1.000000000000000000),
 ( 1.000000000000000000, 0.7071067811865475727, 1.000000000000000000),
 ( 1.000000000000000000, 0.7071067811865475727, 1.000000000000000000),
 ( 1.000000000000000000, 0.7071067811865475727, 1.000000000000000000),
 ( 1.000000000000000000, 0.7071067811865475727, 1.000000000000000000),
 ( 1.000000000000000000, 0.7071067811865475727, 1.000000000000000000) ) ) 
 REPRESENTATION_ITEM ( '' )  SURFACE ( )  );
#86681=CARTESIAN_POINT ( 'NONE',  ( -9.079631412587994888, 13.97901777659653000, 0.000000000000000000 ) ) ;
#86731=CARTESIAN_POINT ( 'NONE',  ( -5.956988534971662475, 4.556784786910193397, -5.000000000000000000 ) ) ;
#86744=DIRECTION ( 'NONE',  ( 1.000000000000000000, 0.000000000000000000, 0.000000000000000000 ) ) ;
#86787=CARTESIAN_POINT ( 'NONE',  ( -3.625510372800185177, 129.4077472144158492, 5.000000000000000000 ) ) ;
#86821=COLOUR_RGB ( '', 0.66274510, 0.83137255, 0.94901961) ;
#86878=FACE_OUTER_BOUND ( 'NONE', #47202, .T. ) ;
#86880=CARTESIAN_POINT ( 'NONE',  ( -7.948255254545235182, 97.89041063984025470, 1.301042606982605321E-15 ) ) ;
#86883=UNCERTAINTY_MEASURE_WITH_UNIT (LENGTH_MEASURE( 1.000000000000000082E-05 ), #92032, 'distance_accuracy_value', 'NONE');
#86955=CARTESIAN_POINT ( 'NONE',  ( -8.985503747028566579, 15.44863866163618304, -5.000000000000635048 ) ) ;
#86979=CARTESIAN_POINT ( 'NONE',  ( -4.315100334823573469, 141.0329282757117824, -5.000000000000000000 ) ) ;
#86980=CARTESIAN_POINT ( 'NONE',  ( 9.517802784862999133, 142.5467050672999676, 0.000000000000000000 ) ) ;
#87063=CARTESIAN_POINT ( 'NONE',  ( 3.225573779814635333, 36.35262730105617379, 4.999999999999998224 ) ) ;
#87094=DIRECTION ( 'NONE',  ( -1.000000000000000000, 0.000000000000000000, 0.000000000000000000 ) ) ;
#87148=DIRECTION ( 'NONE',  ( 0.000000000000000000, 0.000000000000000000, -1.000000000000000000 ) ) ;
#87200=CARTESIAN_POINT ( 'NONE',  ( -3.763170808999132255, 19.48428572230863409, 5.000000000000000888 ) ) ;
#87233=ORIENTED_EDGE ( 'NONE', *, *, #26824, .T. ) ;
#87409=CARTESIAN_POINT ( 'NONE',  ( -8.421452989284619051, 123.3367927118327714, -8.987673073807111741E-31 ) ) ;
#87477=CARTESIAN_POINT ( 'NONE',  ( -5.043779463085778403, 6.427503865159613916, -5.000000000000000000 ) ) ;
#87504=CARTESIAN_POINT ( 'NONE',  ( 8.167402502818406518, 112.7203465494857966, -5.000000000000000888 ) ) ;
#87534=ORIENTED_EDGE ( 'NONE', *, *, #54077, .F. ) ;
#87537=AXIS2_PLACEMENT_3D ( 'NONE', #83509, #8557, #33395 ) ;
#87587=CARTESIAN_POINT ( 'NONE',  ( 3.021265037602210324, 47.67867182518293134, 5.000000000000001776 ) ) ;
#87638=ADVANCED_FACE ( 'NONE', ( #1760 ), #59455, .T. ) ;
#87726=EDGE_CURVE ( 'NONE', #37342, #18064, #62836, .T. ) ;
#87730=CARTESIAN_POINT ( 'NONE',  ( -9.316042626968680906, 11.20129626819939617, -3.173958893453993444E-13 ) ) ;
#87750=( NAMED_UNIT ( * ) SI_UNIT ( $, .STERADIAN. ) SOLID_ANGLE_UNIT ( ) );
#87771=CARTESIAN_POINT ( 'NONE',  ( 4.474408960159398596, 142.5175018677392416, -5.000000000000000000 ) ) ;
#87793=CARTESIAN_POINT ( 'NONE',  ( -0.000000000000000000, 0.000000000000000000, -5.000000000000000000 ) ) ;
#87836=CARTESIAN_POINT ( 'NONE',  ( -2.880896649345847216, 62.46336717673360539, 4.999999999999999112 ) ) ;
#87854=CARTESIAN_POINT ( 'NONE',  ( 6.231493956936422940, 4.173545622688802581, 5.000000000000000000 ) ) ;
#87866=FILL_AREA_STYLE_COLOUR ( '', #92839 ) ;
#87876=( LENGTH_UNIT ( ) NAMED_UNIT ( * ) SI_UNIT ( .MILLI., .METRE. ) );
#87919=APPLICATION_CONTEXT ( 'automotive_design' ) ;
#87925=PRESENTATION_STYLE_ASSIGNMENT (( #104089 ) ) ;
#87977=CARTESIAN_POINT ( 'NONE',  ( 8.427920798850724537, 123.5502821094338941, 0.000000000000000000 ) ) ;
#88001=CARTESIAN_POINT ( 'NONE',  ( -8.066622878784276196, 44.48464632161616805, -5.000000000000000888 ) ) ;
#88010=SURFACE_SIDE_STYLE ('',( #71800 ) ) ;
#88026=DIRECTION ( 'NONE',  ( 0.8308658609248535942, -0.5564727496918441263, 0.000000000000000000 ) ) ;
#88033=CARTESIAN_POINT ( 'NONE',  ( 2.869473476660086675, 64.67010818586889798, -5.000000000000000000 ) ) ;
#88093=CARTESIAN_POINT ( 'NONE',  ( 8.167402502809283149, 39.27965345049499746, -1.228220045931598409E-12 ) ) ;
#88114=VERTEX_POINT ( 'NONE', #7468 ) ;
#88205=DIRECTION ( 'NONE',  ( -1.000000000000000000, 8.881784197001252323E-16, 0.000000000000000000 ) ) ;
#88222=TOROIDAL_SURFACE ( 'NONE', #98508, 7.500000000000006217, 5.000000000000000000 ) ;
#88254=CARTESIAN_POINT ( 'NONE',  ( -4.339355498967208291, 10.71439286440603489, 4.999999999999999112 ) ) ;
#88369=CARTESIAN_POINT ( 'NONE',  ( -4.557632849694865484, 143.2011664447169892, 5.000000000000000000 ) ) ;
#88370=ORIENTED_EDGE ( 'NONE', *, *, #81791, .F. ) ;
#88409=CARTESIAN_POINT ( 'NONE',  ( 14.54015256618498775, 9.738273119607207207, 0.000000000000000000 ) ) ;
#88440=CIRCLE ( 'NONE', #72853, 5.000000000000000000 ) ;
#88468=EDGE_LOOP ( 'NONE', ( #72825, #61757 ) ) ;
#88482=AXIS2_PLACEMENT_3D ( 'NONE', #72596, #46217, #79105 ) ;
#88506=CARTESIAN_POINT ( 'NONE',  ( 8.350191400314127321, 31.24596923992393016, -1.301042606982604532E-15 ) ) ;
#88530=CARTESIAN_POINT ( 'NONE',  ( -4.678819457397887405, 143.9212778189118751, -5.000000000000000000 ) ) ;
#88547=DIRECTION ( 'NONE',  ( -0.000000000000000000, -0.000000000000000000, 1.000000000000000000 ) ) ;
#88558=CARTESIAN_POINT ( 'NONE',  ( 9.240146679348617553, 12.02903014932230263, -5.000000000000000888 ) ) ;
#88692=AXIS2_PLACEMENT_3D ( 'NONE', #51380, #83748, #2290 ) ;
#88728=FILL_AREA_STYLE_COLOUR ( '', #25880 ) ;
#88763=EDGE_CURVE ( 'NONE', #94076, #24323, #52719, .T. ) ;
#88779=CARTESIAN_POINT ( 'NONE',  ( -9.996167984729328992, 7.505519767357340832, 4.999999999999980460 ) ) ;
#88826=SURFACE_STYLE_USAGE ( .BOTH. , #106595 ) ;
#88984=CARTESIAN_POINT ( 'NONE',  ( -9.852227633834194975, 7.822462047239422844, 0.000000000000000000 ) ) ;
#89058=CARTESIAN_POINT ( 'NONE',  ( -3.205024334892935478, 114.6873541103733203, -4.999999999999999112 ) ) ;
#89088=CARTESIAN_POINT ( 'NONE',  ( 8.642300018710525222, 22.39467290678391009, 1.228393653933357778E-12 ) ) ;
#89154=ORIENTED_EDGE ( 'NONE', *, *, #104735, .T. ) ;
#89156=CIRCLE ( 'NONE', #102945, 7.500000000000006217 ) ;
#89358=PRESENTATION_STYLE_ASSIGNMENT (( #48339 ) ) ;
#89389=TOROIDAL_SURFACE ( 'NONE', #99685, 7.500000000000000888, 5.000000000000000000 ) ;
#89427=CARTESIAN_POINT ( 'NONE',  ( -4.839255126185086020, 7.222890253225617840, 5.000000000000000000 ) ) ;
#89442=CYLINDRICAL_SURFACE ( 'NONE', #98058, 5.000000000000000888 ) ;
#89589=CARTESIAN_POINT ( 'NONE',  ( -4.313686681661103250, 141.0184800401511325, -5.000000000000000888 ) ) ;
#89620=CARTESIAN_POINT ( 'NONE',  ( 8.020869781902053575, 47.74450561243712343, -5.000000000000000888 ) ) ;
#89682=CARTESIAN_POINT ( 'NONE',  ( 8.986743721226838844, 15.43298062744137056, -6.150437581724646990E-13 ) ) ;
#89755=( NAMED_UNIT ( * ) SI_UNIT ( $, .STERADIAN. ) SOLID_ANGLE_UNIT ( ) );
#89839=CARTESIAN_POINT ( 'NONE',  ( -10.00002837221254559, 7.499959371255492613, 0.000000000000000000 ) ) ;
#89882=CARTESIAN_POINT ( 'NONE',  ( 3.996139059897768409, 136.8746867953503852, -5.000000000000000888 ) ) ;
#89889=FILL_AREA_STYLE ('',( #39758 ) ) ;
#89962=CARTESIAN_POINT ( 'NONE',  ( -9.609486011791419813, 143.0915023496522451, 5.000000000000004441 ) ) ;
#89988=EDGE_CURVE ( 'NONE', #33529, #98095, #4927, .T. ) ;
#90099=DIRECTION ( 'NONE',  ( -1.000000000000000000, 0.000000000000000000, 0.000000000000000000 ) ) ;
#90109=CARTESIAN_POINT ( 'NONE',  ( -7.844405524234906224, 79.54154322733928950, 0.000000000000000000 ) ) ;
#90128=CARTESIAN_POINT ( 'NONE',  ( 4.678819457397437986, 8.078722181090837395, 5.000000000000000000 ) ) ;
#90144=CARTESIAN_POINT ( 'NONE',  ( 9.439578326262742181, 10.07476781607968341, -4.999999999999079847 ) ) ;
#90247=FILL_AREA_STYLE_COLOUR ( '', #63067 ) ;
#90275=ORIENTED_EDGE ( 'NONE', *, *, #28052, .T. ) ;
#90311=DIRECTION ( 'NONE',  ( -1.000000000000000000, 0.000000000000000000, 0.000000000000000000 ) ) ;
#90362=CARTESIAN_POINT ( 'NONE',  ( -10.11206553723566159, 7.339953826372351386, 0.000000000000000000 ) ) ;
#90424=( NAMED_UNIT ( * ) PLANE_ANGLE_UNIT ( ) SI_UNIT ( $, .RADIAN. ) );
#90460=TOROIDAL_SURFACE ( 'NONE', #105910, 10.00000000000000000, 5.000000000000000000 ) ;
#90480=CARTESIAN_POINT ( 'NONE',  ( -4.404139836249539641, 10.09840216323677708, 5.000000000000000888 ) ) ;
#90494=CARTESIAN_POINT ( 'NONE',  ( -9.291504855474395086, 140.5441818688510693, 6.367976583174694128E-13 ) ) ;
#90549=DIRECTION ( 'NONE',  ( -0.000000000000000000, -0.000000000000000000, 1.000000000000000000 ) ) ;
#90576=ADVANCED_FACE ( 'NONE', ( #56513 ), #89442, .F. ) ;
#90646=DIRECTION ( 'NONE',  ( -0.000000000000000000, -0.000000000000000000, 1.000000000000000000 ) ) ;
#90741=CARTESIAN_POINT ( 'NONE',  ( 7.849089830966804904, 81.65314728018610424, 5.000000000002456702 ) ) ;
#90813=CARTESIAN_POINT ( 'NONE',  ( -5.479219201945285889, 5.339799775453948349, -5.000000000000000888 ) ) ;
#90818=SURFACE_STYLE_FILL_AREA ( #106447 ) ;
#90864=ADVANCED_FACE ( 'NONE', ( #15406 ), #63992, .F. ) ;
#90906=CARTESIAN_POINT ( 'NONE',  ( -5.914126066640156942, 4.617998735621883455, 4.999999999999999112 ) ) ;
#90930=CARTESIAN_POINT ( 'NONE',  ( 0.000000000000000000, 0.000000000000000000, 5.000000000000000000 ) ) ;
#90959=CARTESIAN_POINT ( 'NONE',  ( 3.363233428609735398, 30.69038356566756676, -4.999999999999999112 ) ) ;
#91113=VERTEX_POINT ( 'NONE', #78421 ) ;
#91197=SURFACE_SIDE_STYLE ('',( #25965 ) ) ;
#91247=DIRECTION ( 'NONE',  ( -0.000000000000000000, -0.000000000000000000, -1.000000000000000000 ) ) ;
#91276=( GEOMETRIC_REPRESENTATION_CONTEXT ( 3 ) GLOBAL_UNCERTAINTY_ASSIGNED_CONTEXT ( ( #22429 ) ) GLOBAL_UNIT_ASSIGNED_CONTEXT ( ( #52356, #21625, #46404 ) ) REPRESENTATION_CONTEXT ( 'NONE', 'WORKASPACE' ) );
#91323=CARTESIAN_POINT ( 'NONE',  ( -5.892146328597755556, 4.649454379198777687, -5.000000000000000000 ) ) ;
#91367=ORIENTED_EDGE ( 'NONE', *, *, #30428, .F. ) ;
#91517=SURFACE_SIDE_STYLE ('',( #58616 ) ) ;
#91556=EDGE_CURVE ( 'NONE', #44531, #88114, #24193, .T. ) ;
#91571=FILL_AREA_STYLE_COLOUR ( '', #7334 ) ;
#91643=FILL_AREA_STYLE ('',( #67368 ) ) ;
#91841=CARTESIAN_POINT ( 'NONE',  ( -5.903805371513020539, 4.632738215795892955, -4.999999999999999112 ) ) ;
#92032=( LENGTH_UNIT ( ) NAMED_UNIT ( * ) SI_UNIT ( .MILLI., .METRE. ) );
#92050=DIRECTION ( 'NONE',  ( 0.000000000000000000, 0.000000000000000000, 1.000000000000000000 ) ) ;
#92063=DIRECTION ( 'NONE',  ( 1.000000000000000000, 0.000000000000000000, 0.000000000000000000 ) ) ;
#92081=CARTESIAN_POINT ( 'NONE',  ( -8.474746145506617978, 26.96279221873722776, 0.000000000000000000 ) ) ;
#92099=DIRECTION ( 'NONE',  ( -0.000000000000000000, -0.000000000000000000, -1.000000000000000000 ) ) ;
#92214=AXIS2_PLACEMENT_3D ( 'NONE', #13579, #79911, #6547 ) ;
#92336=CARTESIAN_POINT ( 'NONE',  ( 4.678819457397437986, 8.078722181090837395, 0.000000000000000000 ) ) ;
#92353=CARTESIAN_POINT ( 'NONE',  ( -5.912155184616126213, 4.620813446856026019, -4.999999999999999112 ) ) ;
#92450=EDGE_CURVE ( 'NONE', #97405, #36785, #13964, .T. ) ;
#92507=ORIENTED_EDGE ( 'NONE', *, *, #76700, .F. ) ;
#92614=CARTESIAN_POINT ( 'NONE',  ( -8.309329435564448474, 32.78459446882924766, 0.000000000000000000 ) ) ;
#92661=CIRCLE ( 'NONE', #35893, 5.000000000000002665 ) ;
#92718=CARTESIAN_POINT ( 'NONE',  ( 2.869468778192031166, 64.67094895189187298, 5.000000000000000000 ) ) ;
#92751=MECHANICAL_DESIGN_GEOMETRIC_PRESENTATION_REPRESENTATION('',(#106527),#3219);
#92784=MECHANICAL_DESIGN_GEOMETRIC_PRESENTATION_REPRESENTATION('',(#101422),#104805);
#92839=COLOUR_RGB ( '', 0.40784314, 0.44705882, 0.49803922) ;
#92894=CARTESIAN_POINT ( 'NONE',  ( -9.999565592957996074, 7.500620397551100105, -4.999999999999999112 ) ) ;
#92909=FILL_AREA_STYLE_COLOUR ( '', #47341 ) ;
#93079=ADVANCED_FACE ( 'NONE', ( #94969, #20596, #13477 ), #45350, .F. ) ;
#93157=CARTESIAN_POINT ( 'NONE',  ( -7.860264365984205526, 85.36576122646903286, 0.000000000000000000 ) ) ;
#93231=SURFACE_STYLE_FILL_AREA ( #91643 ) ;
#93259=CARTESIAN_POINT ( 'NONE',  ( 8.361479372611764660, 121.1764542251195280, 5.000000000001228351 ) ) ;
#93311=FACE_OUTER_BOUND ( 'NONE', #29053, .T. ) ;
#93329=ORIENTED_EDGE ( 'NONE', *, *, #30704, .T. ) ;
#93400=ADVANCED_FACE ( 'NONE', ( #18299 ), #88222, .T. ) ;
#93445=( NAMED_UNIT ( * ) SI_UNIT ( $, .STERADIAN. ) SOLID_ANGLE_UNIT ( ) );
#93474=CARTESIAN_POINT ( 'NONE',  ( 9.300358455898974697, 140.6343319111079779, 3.070077524146086535E-13 ) ) ;
#93694=CARTESIAN_POINT ( 'NONE',  ( -2.939792614951783900, 97.10348931277984263, 5.000000000000000000 ) ) ;
#93795=CARTESIAN_POINT ( 'NONE',  ( 8.020865862503733013, 47.74483808550601793, 2.456440091863195202E-12 ) ) ;
#93972=CARTESIAN_POINT ( 'NONE',  ( -3.761186937365144090, 19.52715997569687190, -5.000000000000000000 ) ) ;
#93993=CARTESIAN_POINT ( 'NONE',  ( -2.854617081844746718, 68.28765738858956524, -5.000000000000000000 ) ) ;
#94076=VERTEX_POINT ( 'NONE', #16836 ) ;
#94078=CARTESIAN_POINT ( 'NONE',  ( 3.996139059897772405, 15.12531320464965390, 4.999999999999999112 ) ) ;
#94225=CARTESIAN_POINT ( 'NONE',  ( -3.002903359416353002, 102.9618411113580834, 5.000000000000000000 ) ) ;
#94279=CARTESIAN_POINT ( 'NONE',  ( -7.263014275236301387, 5.510894801153387590, -4.742459152899539454 ) ) ;
#94333=CARTESIAN_POINT ( 'NONE',  ( 3.021274963869413188, 104.3221744949810414, 5.000000000000000000 ) ) ;
#94445=CARTESIAN_POINT ( 'NONE',  ( -8.725698932544442954, 131.8165386195289273, -2.602085213965210642E-15 ) ) ;
#94517=CARTESIAN_POINT ( 'NONE',  ( -7.883628181795526935, 62.00818940279086178, -4.999999999999999112 ) ) ;
#94520=ORIENTED_EDGE ( 'NONE', *, *, #49192, .F. ) ;
#94543=CARTESIAN_POINT ( 'NONE',  ( -3.151712658830499780, 111.9492514448680822, -4.999999999999998224 ) ) ;
#94544=CARTESIAN_POINT ( 'NONE',  ( 8.020865862504424015, 104.2551619145339714, 0.000000000000000000 ) ) ;
#94549=CARTESIAN_POINT ( 'NONE',  ( 0.000000000000000000, 152.0000000000000000, 0.000000000000000000 ) ) ;
#94735=CARTESIAN_POINT ( 'NONE',  ( 14.54015256618498775, 9.738273119607207207, 0.000000000000000000 ) ) ;
#94771=CARTESIAN_POINT ( 'NONE',  ( -5.838394382201822275, 4.727980164709353339, 5.000000000000000888 ) ) ;
#94893=AXIS2_PLACEMENT_3D ( 'NONE', #97747, #6093, #63823 ) ;
#94919=( NAMED_UNIT ( * ) PLANE_ANGLE_UNIT ( ) SI_UNIT ( $, .RADIAN. ) );
#94969=FACE_BOUND ( 'NONE', #16068, .T. ) ;
#95042=AXIS2_PLACEMENT_3D ( 'NONE', #10093, #50016, #82920 ) ;
#95047=CARTESIAN_POINT ( 'NONE',  ( -9.686785446502932828, 8.472505610603299431, -5.000000000000000888 ) ) ;
#95071=STYLED_ITEM ( 'NONE', ( #51694 ), #93400 ) ;
#95072=CARTESIAN_POINT ( 'NONE',  ( 3.768804542116022116, 132.6332890310193875, -4.999999999999999112 ) ) ;
#95077=EDGE_CURVE ( 'NONE', #88114, #61174, #88440, .T. ) ;
#95117=EDGE_CURVE ( 'NONE', #74794, #94076, #43808, .T. ) ;
#95152=CARTESIAN_POINT ( 'NONE',  ( 3.641322288960101350, 22.19827187969977089, 4.999999999999997335 ) ) ;
#95185=DIRECTION ( 'NONE',  ( 0.000000000000000000, 0.000000000000000000, -1.000000000000000000 ) ) ;
#95234=ORIENTED_EDGE ( 'NONE', *, *, #2698, .F. ) ;
#95237=SURFACE_SIDE_STYLE ('',( #105439 ) ) ;
#95238=DIRECTION ( 'NONE',  ( 0.000000000000000000, 0.000000000000000000, -1.000000000000000000 ) ) ;
#95259=ADVANCED_FACE ( 'NONE', ( #99082 ), #83194, .T. ) ;
#95288=CARTESIAN_POINT ( 'NONE',  ( -9.999142969094119593, 7.501227345702223381, 0.000000000000000000 ) ) ;
#95389=CARTESIAN_POINT ( 'NONE',  ( -3.006276549692158628, 103.2175972223608937, 4.999999999999999112 ) ) ;
#95393=DIRECTION ( 'NONE',  ( 0.000000000000000000, 0.000000000000000000, 1.000000000000000000 ) ) ;
#95422=( GEOMETRIC_REPRESENTATION_CONTEXT ( 3 ) GLOBAL_UNCERTAINTY_ASSIGNED_CONTEXT ( ( #67773 ) ) GLOBAL_UNIT_ASSIGNED_CONTEXT ( ( #35883, #62652, #39441 ) ) REPRESENTATION_CONTEXT ( 'NONE', 'WORKASPACE' ) );
#95429=EDGE_CURVE ( 'NONE', #80759, #61174, #38337, .T. ) ;
#95535=DIRECTION ( 'NONE',  ( -1.000000000000000000, 0.000000000000000000, 0.000000000000000000 ) ) ;
#95542=DIRECTION ( 'NONE',  ( 0.5564727496918437932, 0.8308658609248540383, -2.895979027895421214E-16 ) ) ;
#95560=CARTESIAN_POINT ( 'NONE',  ( -8.240610721218175172, 35.73638292219670376, -5.000000000000000888 ) ) ;
#95586=PRODUCT_DEFINITION_FORMATION_WITH_SPECIFIED_SOURCE ( 'ANY', '', #53642, .NOT_KNOWN. ) ;
#95589=CARTESIAN_POINT ( 'NONE',  ( -2.942719846374528547, 97.39685729185900698, -5.000000000000000000 ) ) ;
#95590=CARTESIAN_POINT ( 'NONE',  ( 8.441095186813715401, 123.9902009031610817, 0.000000000000000000 ) ) ;
#95760=( LENGTH_UNIT ( ) NAMED_UNIT ( * ) SI_UNIT ( .MILLI., .METRE. ) );
#95801=MECHANICAL_DESIGN_GEOMETRIC_PRESENTATION_REPRESENTATION('',(#52733),#75122);
#95818=CARTESIAN_POINT ( 'NONE',  ( -4.790746215594418267, 7.453269623570716540, 5.000000000000000000 ) ) ;
#95844=AXIS2_PLACEMENT_3D ( 'NONE', #75366, #1467, #5217 ) ;
#95860=CARTESIAN_POINT ( 'NONE',  ( 3.641322288960107567, 129.8017281203003961, -4.999999999999998224 ) ) ;
#95921=CARTESIAN_POINT ( 'NONE',  ( 4.678819457397882964, 143.9212778189118751, 5.000000000000000000 ) ) ;
#95925=CARTESIAN_POINT ( 'NONE',  ( -3.426400788788944496, 123.5889412327351664, 4.999999999999997335 ) ) ;
#95969=PRESENTATION_STYLE_ASSIGNMENT (( #38284 ) ) ;
#96010=ORIENTED_EDGE ( 'NONE', *, *, #89988, .F. ) ;
#96065=CARTESIAN_POINT ( 'NONE',  ( 8.160622567441036423, 39.63602799826242062, -1.301042606982605321E-15 ) ) ;
#96073=SURFACE_STYLE_USAGE ( .BOTH. , #13539 ) ;
#96090=CARTESIAN_POINT ( 'NONE',  ( -9.590509843553020275, 9.008796699642211081, -5.000000000000000888 ) ) ;
#96122=CARTESIAN_POINT ( 'NONE',  ( 7.955551520415933275, 53.39349112219682070, -5.000000000000000888 ) ) ;
#96183=ADVANCED_FACE ( 'NONE', ( #65150 ), #86627, .T. ) ;
#96189=CARTESIAN_POINT ( 'NONE',  ( 3.363266691729805746, 30.68916429454045058, 5.000000000000000888 ) ) ;
#96242=AXIS2_PLACEMENT_3D ( 'NONE', #94549, #70256, #68124 ) ;
#96258=VERTEX_POINT ( 'NONE', #2407 ) ;
#96294=CIRCLE ( 'NONE', #85987, 12.50000000000000000 ) ;
#96306=( NAMED_UNIT ( * ) PLANE_ANGLE_UNIT ( ) SI_UNIT ( $, .RADIAN. ) );
#96307=CARTESIAN_POINT ( 'NONE',  ( 0.000000000000000000, 0.000000000000000000, 0.000000000000000000 ) ) ;
#96356=CARTESIAN_POINT ( 'NONE',  ( -3.574667317769504749, 23.87472662520894318, 5.000000000000000888 ) ) ;
#96399=SURFACE_SIDE_STYLE ('',( #63500 ) ) ;
#96599=CARTESIAN_POINT ( 'NONE',  ( 7.953367043448346330, 98.37964251781980352, -0.000000000000000000 ) ) ;
#96619=CARTESIAN_POINT ( 'NONE',  ( -8.203969886189964811, 114.5837526205014285, -5.000000000002539302 ) ) ;
#96650=CARTESIAN_POINT ( 'NONE',  ( 8.588478090849999802, 23.79665183991622257, 6.142597166387020528E-13 ) ) ;
#96712=CARTESIAN_POINT ( 'NONE',  ( 8.224453817209493423, 36.45934599358590589, 0.000000000000000000 ) ) ;
#96740=CARTESIAN_POINT ( 'NONE',  ( 3.757222014067413518, 132.6327721420962575, 4.999999999999999112 ) ) ;
#96821=ORIENTED_EDGE ( 'NONE', *, *, #35676, .T. ) ;
#96825=SURFACE_STYLE_USAGE ( .BOTH. , #95237 ) ;
#96870=CARTESIAN_POINT ( 'NONE',  ( -9.426441968457679010, 10.21013571248348839, 1.586979446726977284E-13 ) ) ;
#96874=ORIENTED_EDGE ( 'NONE', *, *, #105938, .T. ) ;
#97036=MECHANICAL_DESIGN_GEOMETRIC_PRESENTATION_REPRESENTATION('',(#69499),#78108);
#97062=UNCERTAINTY_MEASURE_WITH_UNIT (LENGTH_MEASURE( 1.000000000000000082E-05 ), #102514, 'distance_accuracy_value', 'NONE');
#97133=CARTESIAN_POINT ( 'NONE',  ( -8.420691126345804634, 123.3228360287961607, -1.270215581529552804E-12 ) ) ;
#97155=ORIENTED_EDGE ( 'NONE', *, *, #81791, .T. ) ;
#97161=CARTESIAN_POINT ( 'NONE',  ( 3.021274963871837915, 47.67782550506024108, -5.000000000000000000 ) ) ;
#97187=CIRCLE ( 'NONE', #47290, 5.000000000000000000 ) ;
#97223=CARTESIAN_POINT ( 'NONE',  ( 9.300358455900566312, 11.36566808887731739, -9.192885337679628000E-13 ) ) ;
#97338=DIRECTION ( 'NONE',  ( 0.000000000000000000, 0.000000000000000000, -1.000000000000000000 ) ) ;
#97371=STYLED_ITEM ( 'NONE', ( #9251 ), #9496 ) ;
#97376=STYLED_ITEM ( 'NONE', ( #32203 ), #56902 ) ;
#97405=VERTEX_POINT ( 'NONE', #29879 ) ;
#97466=ADVANCED_FACE ( 'NONE', ( #35859 ), #9393, .T. ) ;
#97653=CARTESIAN_POINT ( 'NONE',  ( -7.844405524230078086, 79.54154322733928950, -4.999999999994920508 ) ) ;
#97688=CARTESIAN_POINT ( 'NONE',  ( 9.518114776853952463, 9.451441023381173423, 3.089571038418899033E-13 ) ) ;
#97747=CARTESIAN_POINT ( 'NONE',  ( 0.000000000000000000, 152.0000000000000000, -5.000000000000000000 ) ) ;
#97773=SURFACE_SIDE_STYLE ('',( #80528 ) ) ;
#97788=PRODUCT_CONTEXT ( 'NONE', #43806, 'mechanical' ) ;
#97815=EDGE_LOOP ( 'NONE', ( #66849, #70712, #53220, #105874 ) ) ;
#97880=EDGE_CURVE ( 'NONE', #83314, #76218, #62722, .T. ) ;
#97932=CARTESIAN_POINT ( 'NONE',  ( -9.973775868872957417, 7.480993720211312592, 0.6548301084105181413 ) ) ;
#97971=PRESENTATION_STYLE_ASSIGNMENT (( #22530 ) ) ;
#98058=AXIS2_PLACEMENT_3D ( 'NONE', #74296, #29776, #15532 ) ;
#98095=VERTEX_POINT ( 'NONE', #99346 ) ;
#98139=VERTEX_POINT ( 'NONE', #50284 ) ;
#98160=DIRECTION ( 'NONE',  ( 0.000000000000000000, 0.000000000000000000, -1.000000000000000000 ) ) ;
#98165=EDGE_CURVE ( 'NONE', #12822, #31480, #97187, .T. ) ;
#98185=CARTESIAN_POINT ( 'NONE',  ( 14.54015256618498242, 142.2617268803927288, -5.000000000000000000 ) ) ;
#98196=CARTESIAN_POINT ( 'NONE',  ( -7.939742226425032356, 97.07168777238570101, -5.000000000007622347 ) ) ;
#98229=CARTESIAN_POINT ( 'NONE',  ( 8.441132293785429397, 28.00851920974988118, -1.228519433277404106E-12 ) ) ;
#98292=FILL_AREA_STYLE_COLOUR ( '', #12649 ) ;
#98447=CARTESIAN_POINT ( 'NONE',  ( -10.41860328468742658, 6.902172553357893037, 0.000000000000000000 ) ) ;
#98457=CARTESIAN_POINT ( 'NONE',  ( -9.864698715442679955, 7.401921974702807994, 1.292231847184868609 ) ) ;
#98499=CARTESIAN_POINT ( 'NONE',  ( 7.849088363683611291, 76.00000000000000000, -5.000000000000000000 ) ) ;
#98508=AXIS2_PLACEMENT_3D ( 'NONE', #43610, #76502, #2611 ) ;
#98515=AXIS2_PLACEMENT_3D ( 'NONE', #69839, #104311, #80030 ) ;
#98556=CARTESIAN_POINT ( 'NONE',  ( -5.749819765084808409, 4.859478910914223349, 5.000000000000001776 ) ) ;
#98574=( LENGTH_UNIT ( ) NAMED_UNIT ( * ) SI_UNIT ( .MILLI., .METRE. ) );
#98580=AXIS2_PLACEMENT_3D ( 'NONE', #106380, #10350, #98821 ) ;
#98713=CARTESIAN_POINT ( 'NONE',  ( -9.291918545211730773, 140.5484994665884244, -5.000000000000000888 ) ) ;
#98809=CARTESIAN_POINT ( 'NONE',  ( 7.955551520411029642, 98.60650887776560580, 5.000000000000000888 ) ) ;
#98821=DIRECTION ( 'NONE',  ( -1.000000000000000000, 0.000000000000000000, 0.000000000000000000 ) ) ;
#98822=ORIENTED_EDGE ( 'NONE', *, *, #41428, .F. ) ;
#98876=FACE_OUTER_BOUND ( 'NONE', #31214, .T. ) ;
#99082=FACE_OUTER_BOUND ( 'NONE', #53046, .T. ) ;
#99095=PRESENTATION_STYLE_ASSIGNMENT (( #83457 ) ) ;
#99269=ORIENTED_EDGE ( 'NONE', *, *, #95429, .T. ) ;
#99346=CARTESIAN_POINT ( 'NONE',  ( -7.500000000000001776, 0.000000000000000000, -5.000000000000000000 ) ) ;
#99375=CARTESIAN_POINT ( 'NONE',  ( -5.938874586546019962, 4.582654186248475980, -4.999999999999999112 ) ) ;
#99503=CARTESIAN_POINT ( 'NONE',  ( -6.322843063242285844, 4.034290371602571312, 5.000000000000000888 ) ) ;
#99518=CARTESIAN_POINT ( 'NONE',  ( -5.956988534971662475, 4.556784786910193397, 5.000000000000000000 ) ) ;
#99581=FILL_AREA_STYLE_COLOUR ( '', #49166 ) ;
#99671=DIRECTION ( 'NONE',  ( -1.224646799147353207E-16, 1.000000000000000000, 0.000000000000000000 ) ) ;
#99685=AXIS2_PLACEMENT_3D ( 'NONE', #38786, #30714, #104027 ) ;
#99920=CARTESIAN_POINT ( 'NONE',  ( -10.00791540606109820, 7.488695628611232280, -4.999999999999999112 ) ) ;
#100054=AXIS2_PLACEMENT_3D ( 'NONE', #67983, #42101, #1627 ) ;
#100120=DIRECTION ( 'NONE',  ( 0.000000000000000000, 0.000000000000000000, -1.000000000000000000 ) ) ;
#100160=DIRECTION ( 'NONE',  ( 0.000000000000000000, 0.000000000000000000, -1.000000000000000000 ) ) ;
#100174=CARTESIAN_POINT ( 'NONE',  ( -8.203754751761275443, 114.5734753959365975, 5.000000000000000000 ) ) ;
#100456=CARTESIAN_POINT ( 'NONE',  ( -9.969369542538062845, 7.546308885167836600, -5.000000000000000888 ) ) ;
#100457=EDGE_CURVE ( 'NONE', #24323, #33529, #35562, .T. ) ;
#100551=MECHANICAL_DESIGN_GEOMETRIC_PRESENTATION_REPRESENTATION('',(#36844),#43731);
#100577=TOROIDAL_SURFACE ( 'NONE', #54055, 7.500000000000000888, 5.000000000000000000 ) ;
#100625=CARTESIAN_POINT ( 'NONE',  ( 4.086341046824178314, 13.71216495598962304, -5.000000000000001776 ) ) ;
#100700=CARTESIAN_POINT ( 'NONE',  ( -7.844366129626889617, 79.51894426619178091, 0.000000000000000000 ) ) ;
#100736=DIRECTION ( 'NONE',  ( -0.000000000000000000, -0.000000000000000000, -1.000000000000000000 ) ) ;
#100777=( NAMED_UNIT ( * ) SI_UNIT ( $, .STERADIAN. ) SOLID_ANGLE_UNIT ( ) );
#100805=CARTESIAN_POINT ( 'NONE',  ( 9.075140001324529138, 137.9474095044899968, 6.144345929921320785E-13 ) ) ;
#100843=( GEOMETRIC_REPRESENTATION_CONTEXT ( 3 ) GLOBAL_UNCERTAINTY_ASSIGNED_CONTEXT ( ( #80425 ) ) GLOBAL_UNIT_ASSIGNED_CONTEXT ( ( #32744, #90424, #65616 ) ) REPRESENTATION_CONTEXT ( 'NONE', 'WORKASPACE' ) );
#100948=DIRECTION ( 'NONE',  ( -0.000000000000000000, -1.000000000000000000, -0.000000000000000000 ) ) ;
#100987=CARTESIAN_POINT ( 'NONE',  ( -9.969369541356423170, 7.546308884394301586, 0.000000000000000000 ) ) ;
#101015=CARTESIAN_POINT ( 'NONE',  ( -5.747790115924391152, 4.862630607728038790, -5.000000000000000000 ) ) ;
#101094=EDGE_LOOP ( 'NONE', ( #29329, #8994, #57000, #30892 ) ) ;
#101154=FACE_OUTER_BOUND ( 'NONE', #79174, .T. ) ;
#101173=CIRCLE ( 'NONE', #7565, 4.999999999999998224 ) ;
#101210=ORIENTED_EDGE ( 'NONE', *, *, #91556, .F. ) ;
#101255=CARTESIAN_POINT ( 'NONE',  ( -3.750717479518892006, 132.2449738128835577, 5.000000000000000888 ) ) ;
#101319=CARTESIAN_POINT ( 'NONE',  ( -12.50000000000000533, 152.0000000000000000, 0.000000000000000000 ) ) ;
#101353=CARTESIAN_POINT ( 'NONE',  ( 8.763463954874110229, 132.4016268868458326, 5.000000000000000888 ) ) ;
#101422=STYLED_ITEM ( 'NONE', ( #97971 ), #31256 ) ;
#101447=CIRCLE ( 'NONE', #54924, 10.00000000000000000 ) ;
#101528=CARTESIAN_POINT ( 'NONE',  ( -9.999342726577260976, 7.500940813888675507, 0.000000000000000000 ) ) ;
#101554=CARTESIAN_POINT ( 'NONE',  ( -3.547914663864637497, 24.63190979035525885, -5.000000000000000000 ) ) ;
#101642=FILL_AREA_STYLE_COLOUR ( '', #86821 ) ;
#101689=DIRECTION ( 'NONE',  ( -1.000000000000000000, 0.000000000000000000, 0.000000000000000000 ) ) ;
#101756=CARTESIAN_POINT ( 'NONE',  ( 14.54015256618498775, 9.738273119607207207, 5.000000000000000000 ) ) ;
#101773=CARTESIAN_POINT ( 'NONE',  ( -3.422569409892814551, 123.4621055364969919, 5.000000000000000888 ) ) ;
#101875=CARTESIAN_POINT ( 'NONE',  ( 8.167412539206976518, 112.7208733012430741, 4.999999999998771649 ) ) ;
#101975=CARTESIAN_POINT ( 'NONE',  ( -9.613206415764745216, 8.856620616597396634, 0.000000000000000000 ) ) ;
#102044=CARTESIAN_POINT ( 'NONE',  ( -8.824767335732170537, 18.31512251393273161, -4.999999999999364952 ) ) ;
#102064=SURFACE_SIDE_STYLE ('',( #35237 ) ) ;
#102073=CARTESIAN_POINT ( 'NONE',  ( 9.075061003900238177, 137.9460510617556679, -5.000000000000000888 ) ) ;
#102253=( NAMED_UNIT ( * ) SI_UNIT ( $, .STERADIAN. ) SOLID_ANGLE_UNIT ( ) );
#102306=CARTESIAN_POINT ( 'NONE',  ( -4.248277208370227598, 140.2847170224943056, 4.999999999999997335 ) ) ;
#102414=CARTESIAN_POINT ( 'NONE',  ( 8.588478090850260926, 128.2033481600911955, 6.133923549007229389E-13 ) ) ;
#102493=DIRECTION ( 'NONE',  ( -1.000000000000000000, 0.000000000000000000, 0.000000000000000000 ) ) ;
#102514=( LENGTH_UNIT ( ) NAMED_UNIT ( * ) SI_UNIT ( .MILLI., .METRE. ) );
#102522=CARTESIAN_POINT ( 'NONE',  ( -9.826266471807617364, 7.906979468790463095, -0.000000000000000000 ) ) ;
#102590=CARTESIAN_POINT ( 'NONE',  ( -3.475980472679373268, 26.84355119020046132, -5.000000000000000000 ) ) ;
#102616=CARTESIAN_POINT ( 'NONE',  ( -3.454139446565478888, 27.54133855866839653, -5.000000000000000000 ) ) ;
#102617=CARTESIAN_POINT ( 'NONE',  ( 8.763392006801380418, 132.4000990056166529, -4.999999999999999112 ) ) ;
#102708=( GEOMETRIC_REPRESENTATION_CONTEXT ( 3 ) GLOBAL_UNCERTAINTY_ASSIGNED_CONTEXT ( ( #70946 ) ) GLOBAL_UNIT_ASSIGNED_CONTEXT ( ( #38052, #49807, #89755 ) ) REPRESENTATION_CONTEXT ( 'NONE', 'WORKASPACE' ) );
#102828=ADVANCED_FACE ( 'NONE', ( #81942 ), #86243, .T. ) ;
#102844=CARTESIAN_POINT ( 'NONE',  ( -9.426441968764315504, 10.21013571251764418, 4.999999999999999112 ) ) ;
#102945=AXIS2_PLACEMENT_3D ( 'NONE', #44957, #60087, #44412 ) ;
#102953=CARTESIAN_POINT ( 'NONE',  ( -4.250171846664082764, 140.3062447900153700, 4.999999999999999112 ) ) ;
#103056=CARTESIAN_POINT ( 'NONE',  ( -8.955352252652177825, 136.0524461000850920, -2.602085213965210247E-15 ) ) ;
#103100=CARTESIAN_POINT ( 'NONE',  ( 8.427926236130485194, 28.44948122801527646, 3.851859888774447621E-31 ) ) ;
#103123=CARTESIAN_POINT ( 'NONE',  ( -8.755878939558428442, 19.75811540482035866, -4.999999999999364952 ) ) ;
#103151=CARTESIAN_POINT ( 'NONE',  ( -2.880884120806427084, 62.46550056523758343, -5.000000000000000888 ) ) ;
#103152=CARTESIAN_POINT ( 'NONE',  ( 9.439237903448747247, 141.9224268365072419, -3.070077524146086535E-13 ) ) ;
#103235=CARTESIAN_POINT ( 'NONE',  ( 4.258869285391245540, 11.59559883260999413, 5.000000000000000000 ) ) ;
#103285=FILL_AREA_STYLE ('',( #39621 ) ) ;
#103342=CARTESIAN_POINT ( 'NONE',  ( 10.38582326156068625, 145.0440906288519614, 0.000000000000000000 ) ) ;
#103349=ORIENTED_EDGE ( 'NONE', *, *, #100457, .T. ) ;
#103376=CARTESIAN_POINT ( 'NONE',  ( -9.993721417788709260, 7.509139500089329289, 5.000000000000019540 ) ) ;
#103421=CARTESIAN_POINT ( 'NONE',  ( -5.000000000000002665, 152.0000000000000000, -5.000000000000000000 ) ) ;
#103516=DIRECTION ( 'NONE',  ( 0.000000000000000000, 0.000000000000000000, -1.000000000000000000 ) ) ;
#103571=SURFACE_STYLE_FILL_AREA ( #37820 ) ;
#103574=CARTESIAN_POINT ( 'NONE',  ( -9.041837334944171189, 137.4638978311212725, -1.155557966632342738E-30 ) ) ;
#103644=CARTESIAN_POINT ( 'NONE',  ( -9.076657994649689698, 14.02231722283517534, -4.999999999999365841 ) ) ;
#103675=CARTESIAN_POINT ( 'NONE',  ( 9.439237903996360757, 141.9224268364482668, -4.999999999999999112 ) ) ;
#103888=CARTESIAN_POINT ( 'NONE',  ( -8.826886570201967430, 18.27301070672071148, 4.999999999999999112 ) ) ;
#104027=DIRECTION ( 'NONE',  ( -1.000000000000000000, 0.000000000000000000, 0.000000000000000000 ) ) ;
#104064=VERTEX_POINT ( 'NONE', #55210 ) ;
#104089=SURFACE_STYLE_USAGE ( .BOTH. , #37816 ) ;
#104094=CARTESIAN_POINT ( 'NONE',  ( -7.963455549596985428, 52.64303760444155955, -0.000000000000000000 ) ) ;
#104167=CARTESIAN_POINT ( 'NONE',  ( -9.545014793598884495, 9.306529264753056196, -5.000000000000000888 ) ) ;
#104193=CARTESIAN_POINT ( 'NONE',  ( 4.678819457397414894, 143.9212778189090614, -5.000000000000000888 ) ) ;
#104256=CARTESIAN_POINT ( 'NONE',  ( 8.441095186811990558, 28.00979909688833658, 2.456708350805680174E-12 ) ) ;
#104280=CARTESIAN_POINT ( 'NONE',  ( 4.560915367935576725, 8.779328275237030965, 4.999999999999999112 ) ) ;
#104311=DIRECTION ( 'NONE',  ( 0.000000000000000000, 0.000000000000000000, 1.000000000000000000 ) ) ;
#104418=CARTESIAN_POINT ( 'NONE',  ( -8.826886570334650628, 18.27301070672817573, 6.352460523676195047E-13 ) ) ;
#104464=CARTESIAN_POINT ( 'NONE',  ( 3.168307535684225851, 112.8159850782372047, -5.000000000000000000 ) ) ;
#104471=ORIENTED_EDGE ( 'NONE', *, *, #35706, .F. ) ;
#104473=DIRECTION ( 'NONE',  ( -1.000000000000000000, 0.000000000000000000, -0.000000000000000000 ) ) ;
#104530=VERTEX_POINT ( 'NONE', #64530 ) ;
#104575=ORIENTED_EDGE ( 'NONE', *, *, #98165, .T. ) ;
#104576=DIRECTION ( 'NONE',  ( -1.000000000000000000, 0.000000000000000000, 0.000000000000000000 ) ) ;
#104701=CARTESIAN_POINT ( 'NONE',  ( -8.340816975846024661, 120.4114851255831837, -4.999999999997459810 ) ) ;
#104731=CARTESIAN_POINT ( 'NONE',  ( 3.225607053692172599, 36.35104404975468384, -4.999999999999997335 ) ) ;
#104732=CARTESIAN_POINT ( 'NONE',  ( 7.500000000000000888, 9.184850993605149917E-16, 0.000000000000000000 ) ) ;
#104735=EDGE_CURVE ( 'NONE', #56878, #30328, #36530, .T. ) ;
#104765=CIRCLE ( 'NONE', #87537, 7.500000000000006217 ) ;
#104795=CARTESIAN_POINT ( 'NONE',  ( 4.474494503600904061, 9.481805777968613569, 5.000000000000002665 ) ) ;
#104805=( GEOMETRIC_REPRESENTATION_CONTEXT ( 3 ) GLOBAL_UNCERTAINTY_ASSIGNED_CONTEXT ( ( #4093 ) ) GLOBAL_UNIT_ASSIGNED_CONTEXT ( ( #55373, #23583, #87750 ) ) REPRESENTATION_CONTEXT ( 'NONE', 'WORKASPACE' ) );
#104850=TOROIDAL_SURFACE ( 'NONE', #96242, 7.500000000000006217, 5.000000000000000000 ) ;
#104876=SURFACE_STYLE_USAGE ( .BOTH. , #6157 ) ;
#104967=CARTESIAN_POINT ( 'NONE',  ( -3.997663733872217406, 15.09624604205074938, 4.999999999999999112 ) ) ;
#105100=AXIS2_PLACEMENT_3D ( 'NONE', #75431, #19907, #68421 ) ;
#105151=AXIS2_PLACEMENT_3D ( 'NONE', #75992, #67907, #10714 ) ;
#105157=ORIENTED_EDGE ( 'NONE', *, *, #88763, .T. ) ;
#105180=VERTEX_POINT ( 'NONE', #90128 ) ;
#105193=ORIENTED_EDGE ( 'NONE', *, *, #89988, .T. ) ;
#105213=CARTESIAN_POINT ( 'NONE',  ( 8.017323899013264921, 48.02671738540060176, -1.301042606982606307E-15 ) ) ;
#105240=CARTESIAN_POINT ( 'NONE',  ( -2.939951578610683125, 97.11948718078730280, -5.000000000000002665 ) ) ;
#105266=CARTESIAN_POINT ( 'NONE',  ( 8.020869781911409646, 47.74450561243745739, -2.456496610752231936E-12 ) ) ;
#105329=CARTESIAN_POINT ( 'NONE',  ( 9.239881048102057903, 12.03209342865604548, 5.000000000000307310 ) ) ;
#105335=EDGE_LOOP ( 'NONE', ( #38857, #96874, #53552, #34314 ) ) ;
#105342=CIRCLE ( 'NONE', #95042, 5.000000000000000000 ) ;
#105352=EDGE_CURVE ( 'NONE', #3260, #91113, #26053, .T. ) ;
#105355=CARTESIAN_POINT ( 'NONE',  ( 3.996126808948607056, 136.8744835974398768, 5.000000000000001776 ) ) ;
#105439=SURFACE_STYLE_FILL_AREA ( #71465 ) ;
#105484=CARTESIAN_POINT ( 'NONE',  ( -10.00190353424524226, 7.497281471361841199, 4.999999999999998224 ) ) ;
#105540=CARTESIAN_POINT ( 'NONE',  ( -9.973779925059078622, 7.480996659792954695, -0.6547794009576259899 ) ) ;
#105658=( GEOMETRIC_REPRESENTATION_CONTEXT ( 3 ) GLOBAL_UNCERTAINTY_ASSIGNED_CONTEXT ( ( #65090 ) ) GLOBAL_UNIT_ASSIGNED_CONTEXT ( ( #7699, #6110, #71918 ) ) REPRESENTATION_CONTEXT ( 'NONE', 'WORKASPACE' ) );
#105756=CARTESIAN_POINT ( 'NONE',  ( -8.618528913669065261, 129.1314578643986408, -4.999999999998729017 ) ) ;
#105789=CARTESIAN_POINT ( 'NONE',  ( 8.830661707067434918, 18.20374273969088819, -5.000000000000000888 ) ) ;
#105805=DIRECTION ( 'NONE',  ( -0.000000000000000000, -1.000000000000000000, -0.000000000000000000 ) ) ;
#105870=CARTESIAN_POINT ( 'NONE',  ( 2.955787000303755185, 98.65688599150308846, 5.000000000000000000 ) ) ;
#105874=ORIENTED_EDGE ( 'NONE', *, *, #13911, .F. ) ;
#105910=AXIS2_PLACEMENT_3D ( 'NONE', #1692, #59431, #9781 ) ;
#105938=EDGE_CURVE ( 'NONE', #96258, #106589, #15826, .T. ) ;
#105998=CARTESIAN_POINT ( 'NONE',  ( -10.00190353424524048, 7.497281471361842087, 0.000000000000000000 ) ) ;
#106124=CARTESIAN_POINT ( 'NONE',  ( -9.514607630182533526, 142.5277189163442415, -2.884741510313297714E-12 ) ) ;
#106180=CARTESIAN_POINT ( 'NONE',  ( 6.231493956936422940, 4.173545622688802581, 0.000000000000000000 ) ) ;
#106273=CARTESIAN_POINT ( 'NONE',  ( -2.844395363893353235, 79.54923207833792276, -5.000000000000000000 ) ) ;
#106365=CARTESIAN_POINT ( 'NONE',  ( 3.646183794693278024, 22.19690050403223225, 5.000000000000000000 ) ) ;
#106367=MECHANICAL_DESIGN_GEOMETRIC_PRESENTATION_REPRESENTATION('',(#25419),#4764);
#106380=CARTESIAN_POINT ( 'NONE',  ( 0.000000000000000000, 152.0000000000000000, 0.000000000000000000 ) ) ;
#106391=( NAMED_UNIT ( * ) SI_UNIT ( $, .STERADIAN. ) SOLID_ANGLE_UNIT ( ) );
#106392=AXIS2_PLACEMENT_3D ( 'NONE', #58948, #84277, #30851 ) ;
#106447=FILL_AREA_STYLE ('',( #75680 ) ) ;
#106527=STYLED_ITEM ( 'NONE', ( #3397 ), #41370 ) ;
#106535=CARTESIAN_POINT ( 'NONE',  ( -10.01627249115706775, 7.476760474189256378, 0.000000000000000000 ) ) ;
#106550=CARTESIAN_POINT ( 'NONE',  ( -6.222225870502539280, 4.750888635085242839, 4.991891345689136728 ) ) ;
#106589=VERTEX_POINT ( 'NONE', #27461 ) ;
#106595=SURFACE_SIDE_STYLE ('',( #71566 ) ) ;
#106599=CARTESIAN_POINT ( 'NONE',  ( -9.999999999999982236, 7.499999999999973355, 0.000000000000000000 ) ) ;
#106648=CARTESIAN_POINT ( 'NONE',  ( -5.956988534971662475, 4.556784786910193397, 5.000000000000000000 ) ) ;
#106759=FILL_AREA_STYLE_COLOUR ( '', #20617 ) ;
ENDSEC;
END-ISO-10303-21;
